ISO-10303-21;
HEADER;
/* Generated by software containing ST-Developer
 * from STEP Tools, Inc. (www.steptools.com) 
 */

FILE_DESCRIPTION(
/* description */ (''),
/* implementation_level */ '2;1');

FILE_NAME(
/* name */ 'ISO 4026 - M3 x 6 - 45H (Gib Adjustment Screw).step',
/* time_stamp */ '2026-10-05T09:57:53+05:00',
/* author */ (''),
/* organization */ (''),
/* preprocessor_version */ 'ST-DEVELOPER v20.2',
/* originating_system */ 'Autodesk Translation Framework v15.15.0.0',
/* authorisation */ '');

FILE_SCHEMA (('AUTOMOTIVE_DESIGN { 1 0 10303 214 3 1 1 }'));
ENDSEC;

DATA;
#10=MECHANICAL_DESIGN_GEOMETRIC_PRESENTATION_REPRESENTATION('',(#564),#113984);
#407=(
BOUNDED_CURVE()
B_SPLINE_CURVE(2,(#108240,#108241,#108242),.UNSPECIFIED.,.F.,.F.)
B_SPLINE_CURVE_WITH_KNOTS((3,3),(0.,0.0136874154102654),.UNSPECIFIED.)
CURVE()
GEOMETRIC_REPRESENTATION_ITEM()
RATIONAL_B_SPLINE_CURVE((1.,1.00669106236307,1.00897713805051))
REPRESENTATION_ITEM('')
);
#408=(
BOUNDED_CURVE()
B_SPLINE_CURVE(2,(#108246,#108247,#108248),.UNSPECIFIED.,.F.,.F.)
B_SPLINE_CURVE_WITH_KNOTS((3,3),(0.0278942541126751,0.0415816695229443),
 .UNSPECIFIED.)
CURVE()
GEOMETRIC_REPRESENTATION_ITEM()
RATIONAL_B_SPLINE_CURVE((1.00897713805004,1.00669106236272,1.))
REPRESENTATION_ITEM('')
);
#409=(
BOUNDED_CURVE()
B_SPLINE_CURVE(2,(#108250,#108251,#108252),.UNSPECIFIED.,.F.,.F.)
B_SPLINE_CURVE_WITH_KNOTS((3,3),(0.,0.0136874154102686),.UNSPECIFIED.)
CURVE()
GEOMETRIC_REPRESENTATION_ITEM()
RATIONAL_B_SPLINE_CURVE((1.,1.00669106236263,1.00897713804992))
REPRESENTATION_ITEM('')
);
#410=(
BOUNDED_CURVE()
B_SPLINE_CURVE(2,(#108256,#108257,#108258),.UNSPECIFIED.,.F.,.F.)
B_SPLINE_CURVE_WITH_KNOTS((3,3),(0.0278942541126737,0.04158166952294),
 .UNSPECIFIED.)
CURVE()
GEOMETRIC_REPRESENTATION_ITEM()
RATIONAL_B_SPLINE_CURVE((1.00897713804992,1.00669106236263,1.))
REPRESENTATION_ITEM('')
);
#411=(
BOUNDED_CURVE()
B_SPLINE_CURVE(2,(#108260,#108261,#108262),.UNSPECIFIED.,.F.,.F.)
B_SPLINE_CURVE_WITH_KNOTS((3,3),(0.,0.0136874154102691),.UNSPECIFIED.)
CURVE()
GEOMETRIC_REPRESENTATION_ITEM()
RATIONAL_B_SPLINE_CURVE((1.,1.00669106236264,1.00897713804994))
REPRESENTATION_ITEM('')
);
#412=(
BOUNDED_CURVE()
B_SPLINE_CURVE(2,(#108266,#108267,#108268),.UNSPECIFIED.,.F.,.F.)
B_SPLINE_CURVE_WITH_KNOTS((3,3),(0.0278942541126743,0.0415816695229415),
 .UNSPECIFIED.)
CURVE()
GEOMETRIC_REPRESENTATION_ITEM()
RATIONAL_B_SPLINE_CURVE((1.00897713805037,1.00669106236296,1.))
REPRESENTATION_ITEM('')
);
#413=(
BOUNDED_CURVE()
B_SPLINE_CURVE(2,(#108270,#108271,#108272),.UNSPECIFIED.,.F.,.F.)
B_SPLINE_CURVE_WITH_KNOTS((3,3),(0.,0.0136874154102738),.UNSPECIFIED.)
CURVE()
GEOMETRIC_REPRESENTATION_ITEM()
RATIONAL_B_SPLINE_CURVE((1.,1.00669106236144,1.00897713804833))
REPRESENTATION_ITEM('')
);
#414=(
BOUNDED_CURVE()
B_SPLINE_CURVE(2,(#108276,#108277,#108278),.UNSPECIFIED.,.F.,.F.)
B_SPLINE_CURVE_WITH_KNOTS((3,3),(0.0278942541126704,0.0415816695229415),
 .UNSPECIFIED.)
CURVE()
GEOMETRIC_REPRESENTATION_ITEM()
RATIONAL_B_SPLINE_CURVE((1.00897713804912,1.00669106236203,1.))
REPRESENTATION_ITEM('')
);
#415=(
BOUNDED_CURVE()
B_SPLINE_CURVE(2,(#108280,#108281,#108282),.UNSPECIFIED.,.F.,.F.)
B_SPLINE_CURVE_WITH_KNOTS((3,3),(0.,0.013687415410267),.UNSPECIFIED.)
CURVE()
GEOMETRIC_REPRESENTATION_ITEM()
RATIONAL_B_SPLINE_CURVE((1.,1.0066910623626,1.00897713804988))
REPRESENTATION_ITEM('')
);
#416=(
BOUNDED_CURVE()
B_SPLINE_CURVE(2,(#108286,#108287,#108288),.UNSPECIFIED.,.F.,.F.)
B_SPLINE_CURVE_WITH_KNOTS((3,3),(0.0278942541126708,0.04158166952294),
 .UNSPECIFIED.)
CURVE()
GEOMETRIC_REPRESENTATION_ITEM()
RATIONAL_B_SPLINE_CURVE((1.00897713804988,1.0066910623626,1.))
REPRESENTATION_ITEM('')
);
#417=(
BOUNDED_CURVE()
B_SPLINE_CURVE(2,(#108290,#108291,#108292),.UNSPECIFIED.,.F.,.F.)
B_SPLINE_CURVE_WITH_KNOTS((3,3),(0.,0.0136874154102732),.UNSPECIFIED.)
CURVE()
GEOMETRIC_REPRESENTATION_ITEM()
RATIONAL_B_SPLINE_CURVE((1.,1.00669106236247,1.00897713804971))
REPRESENTATION_ITEM('')
);
#418=(
BOUNDED_CURVE()
B_SPLINE_CURVE(2,(#108295,#108296,#108297),.UNSPECIFIED.,.F.,.F.)
B_SPLINE_CURVE_WITH_KNOTS((3,3),(0.027894254112677,0.0415816695229426),
 .UNSPECIFIED.)
CURVE()
GEOMETRIC_REPRESENTATION_ITEM()
RATIONAL_B_SPLINE_CURVE((1.00897713805068,1.00669106236319,1.))
REPRESENTATION_ITEM('')
);
#528=SHAPE_REPRESENTATION_RELATIONSHIP('SRR','None',#114065,#546);
#546=ADVANCED_BREP_SHAPE_REPRESENTATION('',(#582),#113979);
#564=STYLED_ITEM('',(#114317),#582);
#582=MANIFOLD_SOLID_BREP(
'ISO 4026 - M3 x 6 - 45H (Gib Adjustment Screw)',#60405);
#774=CYLINDRICAL_SURFACE('',#63260,1.4635);
#775=CYLINDRICAL_SURFACE('',#63262,1.4635);
#776=CYLINDRICAL_SURFACE('',#63263,1.4635);
#777=CYLINDRICAL_SURFACE('',#63264,1.4635);
#778=CYLINDRICAL_SURFACE('',#63265,1.4635);
#779=CYLINDRICAL_SURFACE('',#63266,1.4635);
#780=CYLINDRICAL_SURFACE('',#63267,1.4635);
#781=CYLINDRICAL_SURFACE('',#63268,1.4635);
#782=CYLINDRICAL_SURFACE('',#63269,1.4635);
#783=CYLINDRICAL_SURFACE('',#63270,1.4635);
#784=CYLINDRICAL_SURFACE('',#63271,1.4635);
#785=CYLINDRICAL_SURFACE('',#63272,1.17775);
#786=CYLINDRICAL_SURFACE('',#63274,1.17775);
#787=CYLINDRICAL_SURFACE('',#63275,1.17775);
#788=CYLINDRICAL_SURFACE('',#63276,1.17775);
#789=CYLINDRICAL_SURFACE('',#63277,1.17775);
#790=CYLINDRICAL_SURFACE('',#63278,1.17775);
#791=CYLINDRICAL_SURFACE('',#63279,1.17775);
#792=CYLINDRICAL_SURFACE('',#63280,1.17775);
#793=CYLINDRICAL_SURFACE('',#63281,1.17775);
#794=CYLINDRICAL_SURFACE('',#63282,1.17775);
#795=CYLINDRICAL_SURFACE('',#63290,1.17775);
#796=CYLINDRICAL_SURFACE('',#63299,0.816025403784426);
#797=CYLINDRICAL_SURFACE('',#63301,0.816025403784426);
#798=CYLINDRICAL_SURFACE('',#63303,0.816025403784426);
#799=CYLINDRICAL_SURFACE('',#63305,0.816025403784426);
#800=CYLINDRICAL_SURFACE('',#63307,0.816025403784426);
#801=CYLINDRICAL_SURFACE('',#63309,0.816025403784426);
#802=CYLINDRICAL_SURFACE('',#63339,1.4635);
#941=CONICAL_SURFACE('',#63291,0.916025403784424,0.785398163397484);
#942=CONICAL_SURFACE('',#63332,0.866025403784434,1.02974425867665);
#943=CONICAL_SURFACE('',#63338,1.34999999999998,0.785398163397437);
#944=CONICAL_SURFACE('',#63341,1.25,0.785398163397439);
#1361=CIRCLE('',#63261,1.4635);
#1362=CIRCLE('',#63273,1.17775);
#1363=CIRCLE('',#63284,1.4635);
#1364=CIRCLE('',#63285,1.4635);
#1365=CIRCLE('',#63287,1.4635);
#1366=CIRCLE('',#63288,1.4635);
#1367=CIRCLE('',#63289,1.17775);
#1368=CIRCLE('',#63292,1.01602540378443);
#1369=CIRCLE('',#63293,0.816025403784426);
#1370=CIRCLE('',#63294,0.816025403784426);
#1371=CIRCLE('',#63295,0.816025403784426);
#1372=CIRCLE('',#63296,0.816025403784426);
#1373=CIRCLE('',#63297,0.816025403784426);
#1374=CIRCLE('',#63298,0.816025403784426);
#1375=CIRCLE('',#63300,0.816025403784426);
#1376=CIRCLE('',#63302,0.816025403784426);
#1377=CIRCLE('',#63304,0.816025403784426);
#1378=CIRCLE('',#63306,0.816025403784426);
#1379=CIRCLE('',#63308,0.816025403784426);
#1380=CIRCLE('',#63310,0.816025403784426);
#1381=CIRCLE('',#63321,0.866025403784434);
#1382=CIRCLE('',#63323,0.866025403784434);
#1383=CIRCLE('',#63325,0.866025403784434);
#1384=CIRCLE('',#63327,0.866025403784434);
#1385=CIRCLE('',#63329,0.866025403784434);
#1386=CIRCLE('',#63331,0.866025403784434);
#1387=CIRCLE('',#63337,1.19999999999999);
#1388=CIRCLE('',#63340,1.4635);
#1389=CIRCLE('',#63342,0.999999999999996);
#1854=FACE_BOUND('',#10609,.T.);
#3837=PLANE('',#63283);
#3838=PLANE('',#63286);
#3839=PLANE('',#63311);
#3840=PLANE('',#63312);
#3841=PLANE('',#63313);
#3842=PLANE('',#63314);
#3843=PLANE('',#63315);
#3844=PLANE('',#63316);
#3845=PLANE('',#63317);
#3846=PLANE('',#63318);
#3847=PLANE('',#63319);
#3848=PLANE('',#63320);
#3849=PLANE('',#63322);
#3850=PLANE('',#63324);
#3851=PLANE('',#63326);
#3852=PLANE('',#63328);
#3853=PLANE('',#63330);
#3854=PLANE('',#63333);
#3855=PLANE('',#63334);
#3856=PLANE('',#63335);
#3857=PLANE('',#63336);
#3858=PLANE('',#63343);
#6977=FACE_OUTER_BOUND('',#10556,.T.);
#6978=FACE_OUTER_BOUND('',#10557,.T.);
#6979=FACE_OUTER_BOUND('',#10558,.T.);
#6980=FACE_OUTER_BOUND('',#10559,.T.);
#6981=FACE_OUTER_BOUND('',#10560,.T.);
#6982=FACE_OUTER_BOUND('',#10561,.T.);
#6983=FACE_OUTER_BOUND('',#10562,.T.);
#6984=FACE_OUTER_BOUND('',#10563,.T.);
#6985=FACE_OUTER_BOUND('',#10564,.T.);
#6986=FACE_OUTER_BOUND('',#10565,.T.);
#6987=FACE_OUTER_BOUND('',#10566,.T.);
#6988=FACE_OUTER_BOUND('',#10567,.T.);
#6989=FACE_OUTER_BOUND('',#10568,.T.);
#6990=FACE_OUTER_BOUND('',#10569,.T.);
#6991=FACE_OUTER_BOUND('',#10570,.T.);
#6992=FACE_OUTER_BOUND('',#10571,.T.);
#6993=FACE_OUTER_BOUND('',#10572,.T.);
#6994=FACE_OUTER_BOUND('',#10573,.T.);
#6995=FACE_OUTER_BOUND('',#10574,.T.);
#6996=FACE_OUTER_BOUND('',#10575,.T.);
#6997=FACE_OUTER_BOUND('',#10576,.T.);
#6998=FACE_OUTER_BOUND('',#10577,.T.);
#6999=FACE_OUTER_BOUND('',#10578,.T.);
#7000=FACE_OUTER_BOUND('',#10579,.T.);
#7001=FACE_OUTER_BOUND('',#10580,.T.);
#7002=FACE_OUTER_BOUND('',#10581,.T.);
#7003=FACE_OUTER_BOUND('',#10582,.T.);
#7004=FACE_OUTER_BOUND('',#10583,.T.);
#7005=FACE_OUTER_BOUND('',#10584,.T.);
#7006=FACE_OUTER_BOUND('',#10585,.T.);
#7007=FACE_OUTER_BOUND('',#10586,.T.);
#7008=FACE_OUTER_BOUND('',#10587,.T.);
#7009=FACE_OUTER_BOUND('',#10588,.T.);
#7010=FACE_OUTER_BOUND('',#10589,.T.);
#7011=FACE_OUTER_BOUND('',#10590,.T.);
#7012=FACE_OUTER_BOUND('',#10591,.T.);
#7013=FACE_OUTER_BOUND('',#10592,.T.);
#7014=FACE_OUTER_BOUND('',#10593,.T.);
#7015=FACE_OUTER_BOUND('',#10594,.T.);
#7016=FACE_OUTER_BOUND('',#10595,.T.);
#7017=FACE_OUTER_BOUND('',#10596,.T.);
#7018=FACE_OUTER_BOUND('',#10597,.T.);
#7019=FACE_OUTER_BOUND('',#10598,.T.);
#7020=FACE_OUTER_BOUND('',#10599,.T.);
#7021=FACE_OUTER_BOUND('',#10600,.T.);
#7022=FACE_OUTER_BOUND('',#10601,.T.);
#7023=FACE_OUTER_BOUND('',#10602,.T.);
#7024=FACE_OUTER_BOUND('',#10603,.T.);
#7025=FACE_OUTER_BOUND('',#10604,.T.);
#7026=FACE_OUTER_BOUND('',#10605,.T.);
#7027=FACE_OUTER_BOUND('',#10606,.T.);
#7028=FACE_OUTER_BOUND('',#10607,.T.);
#7029=FACE_OUTER_BOUND('',#10608,.T.);
#7030=FACE_OUTER_BOUND('',#10610,.T.);
#7031=FACE_OUTER_BOUND('',#10611,.T.);
#7032=FACE_OUTER_BOUND('',#10612,.T.);
#7033=FACE_OUTER_BOUND('',#10613,.T.);
#10556=EDGE_LOOP('',(#54725,#54726,#54727,#54728));
#10557=EDGE_LOOP('',(#54729,#54730,#54731,#54732));
#10558=EDGE_LOOP('',(#54733,#54734,#54735,#54736));
#10559=EDGE_LOOP('',(#54737,#54738,#54739,#54740));
#10560=EDGE_LOOP('',(#54741,#54742,#54743,#54744));
#10561=EDGE_LOOP('',(#54745,#54746,#54747,#54748));
#10562=EDGE_LOOP('',(#54749,#54750,#54751,#54752));
#10563=EDGE_LOOP('',(#54753,#54754,#54755,#54756));
#10564=EDGE_LOOP('',(#54757,#54758,#54759,#54760));
#10565=EDGE_LOOP('',(#54761,#54762,#54763,#54764));
#10566=EDGE_LOOP('',(#54765,#54766,#54767,#54768));
#10567=EDGE_LOOP('',(#54769,#54770,#54771,#54772));
#10568=EDGE_LOOP('',(#54773,#54774,#54775,#54776));
#10569=EDGE_LOOP('',(#54777,#54778,#54779,#54780));
#10570=EDGE_LOOP('',(#54781,#54782,#54783,#54784));
#10571=EDGE_LOOP('',(#54785,#54786,#54787,#54788));
#10572=EDGE_LOOP('',(#54789,#54790,#54791,#54792));
#10573=EDGE_LOOP('',(#54793,#54794,#54795,#54796));
#10574=EDGE_LOOP('',(#54797,#54798,#54799,#54800));
#10575=EDGE_LOOP('',(#54801,#54802,#54803,#54804));
#10576=EDGE_LOOP('',(#54805,#54806,#54807,#54808));
#10577=EDGE_LOOP('',(#54809,#54810,#54811,#54812,#54813));
#10578=EDGE_LOOP('',(#54814,#54815,#54816,#54817,#54818,#54819,#54820,#54821,
#54822,#54823,#54824,#54825,#54826,#54827,#54828,#54829,#54830,#54831,#54832,
#54833,#54834,#54835,#54836,#54837,#54838));
#10579=EDGE_LOOP('',(#54839,#54840,#54841,#54842,#54843));
#10580=EDGE_LOOP('',(#54844,#54845,#54846,#54847));
#10581=EDGE_LOOP('',(#54848,#54849,#54850,#54851,#54852,#54853,#54854,#54855,
#54856,#54857,#54858,#54859,#54860,#54861,#54862,#54863,#54864,#54865,#54866,
#54867,#54868,#54869,#54870,#54871,#54872));
#10582=EDGE_LOOP('',(#54873,#54874,#54875,#54876,#54877,#54878,#54879,#54880,
#54881,#54882,#54883,#54884,#54885,#54886,#54887,#54888,#54889,#54890,#54891,
#54892,#54893));
#10583=EDGE_LOOP('',(#54894,#54895,#54896,#54897));
#10584=EDGE_LOOP('',(#54898,#54899,#54900,#54901));
#10585=EDGE_LOOP('',(#54902,#54903,#54904,#54905));
#10586=EDGE_LOOP('',(#54906,#54907,#54908,#54909));
#10587=EDGE_LOOP('',(#54910,#54911,#54912,#54913));
#10588=EDGE_LOOP('',(#54914,#54915,#54916,#54917));
#10589=EDGE_LOOP('',(#54918,#54919,#54920,#54921,#54922,#54923,#54924,#54925));
#10590=EDGE_LOOP('',(#54926,#54927,#54928,#54929,#54930,#54931,#54932,#54933));
#10591=EDGE_LOOP('',(#54934,#54935,#54936,#54937,#54938,#54939,#54940,#54941));
#10592=EDGE_LOOP('',(#54942,#54943));
#10593=EDGE_LOOP('',(#54944,#54945));
#10594=EDGE_LOOP('',(#54946,#54947));
#10595=EDGE_LOOP('',(#54948,#54949));
#10596=EDGE_LOOP('',(#54950,#54951));
#10597=EDGE_LOOP('',(#54952,#54953));
#10598=EDGE_LOOP('',(#54954,#54955));
#10599=EDGE_LOOP('',(#54956,#54957));
#10600=EDGE_LOOP('',(#54958,#54959));
#10601=EDGE_LOOP('',(#54960,#54961));
#10602=EDGE_LOOP('',(#54962,#54963));
#10603=EDGE_LOOP('',(#54964,#54965));
#10604=EDGE_LOOP('',(#54966,#54967,#54968,#54969,#54970,#54971,#54972,#54973));
#10605=EDGE_LOOP('',(#54974,#54975,#54976,#54977,#54978,#54979,#54980,#54981));
#10606=EDGE_LOOP('',(#54982,#54983,#54984,#54985,#54986,#54987,#54988,#54989));
#10607=EDGE_LOOP('',(#54990,#54991,#54992,#54993,#54994,#54995,#54996,#54997));
#10608=EDGE_LOOP('',(#54998));
#10609=EDGE_LOOP('',(#54999));
#10610=EDGE_LOOP('',(#55000,#55001,#55002,#55003,#55004,#55005));
#10611=EDGE_LOOP('',(#55006,#55007,#55008,#55009));
#10612=EDGE_LOOP('',(#55010,#55011,#55012,#55013,#55014,#55015));
#10613=EDGE_LOOP('',(#55016));
#16531=LINE('',#106511,#22565);
#16532=LINE('',#106535,#22566);
#16533=LINE('',#106583,#22567);
#16534=LINE('',#106631,#22568);
#16535=LINE('',#106685,#22569);
#16536=LINE('',#106733,#22570);
#16537=LINE('',#106781,#22571);
#16538=LINE('',#106835,#22572);
#16539=LINE('',#106883,#22573);
#16540=LINE('',#106931,#22574);
#16541=LINE('',#106985,#22575);
#16542=LINE('',#107033,#22576);
#16543=LINE('',#107057,#22577);
#16544=LINE('',#107082,#22578);
#16545=LINE('',#107107,#22579);
#16546=LINE('',#107131,#22580);
#16547=LINE('',#107156,#22581);
#16548=LINE('',#107181,#22582);
#16549=LINE('',#107205,#22583);
#16550=LINE('',#107230,#22584);
#16551=LINE('',#107255,#22585);
#16552=LINE('',#108238,#22586);
#16553=LINE('',#108300,#22587);
#16554=LINE('',#108302,#22588);
#16555=LINE('',#108306,#22589);
#16556=LINE('',#108308,#22590);
#16557=LINE('',#108312,#22591);
#16558=LINE('',#108315,#22592);
#16559=LINE('',#108318,#22593);
#16560=LINE('',#108320,#22594);
#16561=LINE('',#108324,#22595);
#16562=LINE('',#108327,#22596);
#16563=LINE('',#108330,#22597);
#16564=LINE('',#108333,#22598);
#16565=LINE('',#108335,#22599);
#16566=LINE('',#108337,#22600);
#16567=LINE('',#108339,#22601);
#16568=LINE('',#108340,#22602);
#16569=LINE('',#108342,#22603);
#16570=LINE('',#108344,#22604);
#16571=LINE('',#108345,#22605);
#16572=LINE('',#108347,#22606);
#16573=LINE('',#108349,#22607);
#16574=LINE('',#108350,#22608);
#16575=LINE('',#108354,#22609);
#16576=LINE('',#108357,#22610);
#16577=LINE('',#108359,#22611);
#16578=LINE('',#108362,#22612);
#16579=LINE('',#108372,#22613);
#16580=LINE('',#108375,#22614);
#16581=LINE('',#108379,#22615);
#16582=LINE('',#108381,#22616);
#16583=LINE('',#108383,#22617);
#16584=LINE('',#108389,#22618);
#16585=LINE('',#108395,#22619);
#22565=VECTOR('',#74735,1.49999999999999);
#22566=VECTOR('',#74740,1.49999999999999);
#22567=VECTOR('',#74743,1.49999999999999);
#22568=VECTOR('',#74746,1.49999999999999);
#22569=VECTOR('',#74749,1.49999999999999);
#22570=VECTOR('',#74752,1.49999999999999);
#22571=VECTOR('',#74755,1.49999999999999);
#22572=VECTOR('',#74758,1.49999999999999);
#22573=VECTOR('',#74761,1.49999999999999);
#22574=VECTOR('',#74764,1.49999999999999);
#22575=VECTOR('',#74767,1.49999999999999);
#22576=VECTOR('',#74770,1.17775);
#22577=VECTOR('',#74775,1.17775);
#22578=VECTOR('',#74778,1.17775);
#22579=VECTOR('',#74781,1.17775);
#22580=VECTOR('',#74784,1.17775);
#22581=VECTOR('',#74787,1.17775);
#22582=VECTOR('',#74790,1.17775);
#22583=VECTOR('',#74793,1.17775);
#22584=VECTOR('',#74796,1.17775);
#22585=VECTOR('',#74799,1.17775);
#22586=VECTOR('',#74820,0.916025403784424);
#22587=VECTOR('',#74835,10.);
#22588=VECTOR('',#74836,10.);
#22589=VECTOR('',#74841,10.);
#22590=VECTOR('',#74842,10.);
#22591=VECTOR('',#74847,10.);
#22592=VECTOR('',#74850,10.);
#22593=VECTOR('',#74853,10.);
#22594=VECTOR('',#74854,10.);
#22595=VECTOR('',#74859,10.);
#22596=VECTOR('',#74862,10.);
#22597=VECTOR('',#74865,10.);
#22598=VECTOR('',#74868,10.);
#22599=VECTOR('',#74871,10.);
#22600=VECTOR('',#74872,10.);
#22601=VECTOR('',#74873,10.);
#22602=VECTOR('',#74874,10.);
#22603=VECTOR('',#74877,10.);
#22604=VECTOR('',#74878,10.);
#22605=VECTOR('',#74879,10.);
#22606=VECTOR('',#74882,10.);
#22607=VECTOR('',#74883,10.);
#22608=VECTOR('',#74884,10.);
#22609=VECTOR('',#74891,10.);
#22610=VECTOR('',#74896,10.);
#22611=VECTOR('',#74899,10.);
#22612=VECTOR('',#74902,10.);
#22613=VECTOR('',#74919,10.);
#22614=VECTOR('',#74924,10.);
#22615=VECTOR('',#74929,0.866025403784434);
#22616=VECTOR('',#74932,10.);
#22617=VECTOR('',#74935,10.);
#22618=VECTOR('',#74944,1.34999999999998);
#22619=VECTOR('',#74953,1.25);
#24447=B_SPLINE_CURVE_WITH_KNOTS('',3,(#106513,#106514,#106515,#106516,
#106517,#106518,#106519,#106520,#106521,#106522),.UNSPECIFIED.,.F.,.F.,
(4,3,3,4),(-4.09202352044855,-3.96148666219335,-2.97111499664502,-2.07317267331975),
 .UNSPECIFIED.);
#24448=B_SPLINE_CURVE_WITH_KNOTS('',3,(#106525,#106526,#106527,#106528,
#106529,#106530,#106531),.UNSPECIFIED.,.F.,.F.,(4,3,4),(0.,0.990371665548332,
1.12274180646094),.UNSPECIFIED.);
#24449=B_SPLINE_CURVE_WITH_KNOTS('',3,(#106536,#106537,#106538,#106539,
#106540,#106541,#106542,#106543,#106544,#106545,#106546,#106547,#106548,
#106549,#106550,#106551,#106552,#106553,#106554,#106555,#106556,#106557),
 .UNSPECIFIED.,.F.,.F.,(4,3,3,3,3,3,3,4),(-10.3752088276281,-9.90371665548338,
-8.91334498993504,-7.9229733243867,-6.93260165883837,-5.94222999329003,
-4.95185832774169,-4.09202352044855),.UNSPECIFIED.);
#24450=B_SPLINE_CURVE_WITH_KNOTS('',3,(#106558,#106559,#106560,#106561,
#106562,#106563,#106564,#106565,#106566,#106567,#106568,#106569,#106570,
#106571,#106572,#106573,#106574,#106575,#106576,#106577,#106578,#106579),
 .UNSPECIFIED.,.F.,.F.,(4,3,3,3,3,3,3,4),(1.12274180646094,1.98074333109667,
2.97111499664501,3.96148666219335,4.95185832774168,5.94222999329002,6.93260165883836,
7.40592711364053),.UNSPECIFIED.);
#24451=B_SPLINE_CURVE_WITH_KNOTS('',3,(#106584,#106585,#106586,#106587,
#106588,#106589,#106590,#106591,#106592,#106593,#106594,#106595,#106596,
#106597,#106598,#106599,#106600,#106601,#106602,#106603,#106604,#106605),
 .UNSPECIFIED.,.F.,.F.,(4,3,3,3,3,3,3,4),(-16.6583941348077,-15.8459466487734,
-14.8555749832251,-13.8652033176767,-12.8748316521284,-11.8844599865801,
-10.8940883210317,-10.3752088276281),.UNSPECIFIED.);
#24452=B_SPLINE_CURVE_WITH_KNOTS('',3,(#106606,#106607,#106608,#106609,
#106610,#106611,#106612,#106613,#106614,#106615,#106616,#106617,#106618,
#106619,#106620,#106621,#106622,#106623,#106624,#106625,#106626,#106627),
 .UNSPECIFIED.,.F.,.F.,(4,3,3,3,3,3,3,4),(7.40592711364053,7.92297332438669,
8.91334498993503,9.90371665548337,10.8940883210317,11.88445998658,12.8748316521284,
13.6891124208201),.UNSPECIFIED.);
#24453=B_SPLINE_CURVE_WITH_KNOTS('',3,(#106632,#106633,#106634,#106635,
#106636,#106637,#106638,#106639,#106640,#106641,#106642,#106643,#106644,
#106645,#106646,#106647,#106648,#106649,#106650,#106651,#106652,#106653,
#106654,#106655,#106656),.UNSPECIFIED.,.F.,.F.,(4,3,3,3,3,3,3,3,4),(-22.9415794419873,
-22.7785483076118,-21.7881766420634,-20.7978049765151,-19.8074333109668,
-18.8170616454184,-17.8266899798701,-16.8363183143217,-16.6583941348077),
 .UNSPECIFIED.);
#24454=B_SPLINE_CURVE_WITH_KNOTS('',3,(#106657,#106658,#106659,#106660,
#106661,#106662,#106663,#106664,#106665,#106666,#106667,#106668,#106669,
#106670,#106671,#106672,#106673,#106674,#106675,#106676,#106677,#106678,
#106679,#106680,#106681),.UNSPECIFIED.,.F.,.F.,(4,3,3,3,3,3,3,3,4),(13.6891124208201,
13.8652033176767,14.8555749832251,15.8459466487734,16.8363183143217,17.8266899798701,
18.8170616454184,19.8074333109667,19.9722977279997),.UNSPECIFIED.);
#24455=B_SPLINE_CURVE_WITH_KNOTS('',3,(#106686,#106687,#106688,#106689,
#106690,#106691,#106692,#106693,#106694,#106695,#106696,#106697,#106698,
#106699,#106700,#106701,#106702,#106703,#106704,#106705,#106706,#106707),
 .UNSPECIFIED.,.F.,.F.,(4,3,3,3,3,3,3,4),(-29.2247647491669,-28.7207783009018,
-27.7304066353535,-26.7400349698051,-25.7496633042568,-24.7592916387085,
-23.7689199731601,-22.9415794419873),.UNSPECIFIED.);
#24456=B_SPLINE_CURVE_WITH_KNOTS('',3,(#106708,#106709,#106710,#106711,
#106712,#106713,#106714,#106715,#106716,#106717,#106718,#106719,#106720,
#106721,#106722,#106723,#106724,#106725,#106726,#106727,#106728,#106729),
 .UNSPECIFIED.,.F.,.F.,(4,3,3,3,3,3,3,4),(19.9722977279997,20.7978049765151,
21.7881766420634,22.7785483076118,23.7689199731601,24.7592916387084,25.7496633042568,
26.2554830351793),.UNSPECIFIED.);
#24457=B_SPLINE_CURVE_WITH_KNOTS('',3,(#106734,#106735,#106736,#106737,
#106738,#106739,#106740,#106741,#106742,#106743,#106744,#106745,#106746,
#106747,#106748,#106749,#106750,#106751,#106752,#106753,#106754,#106755),
 .UNSPECIFIED.,.F.,.F.,(4,3,3,3,3,3,3,4),(-35.5079500563465,-34.6630082941918,
-33.6726366286435,-32.6822649630952,-31.6918932975468,-30.7015216319985,
-29.7111499664501,-29.2247647491669),.UNSPECIFIED.);
#24458=B_SPLINE_CURVE_WITH_KNOTS('',3,(#106756,#106757,#106758,#106759,
#106760,#106761,#106762,#106763,#106764,#106765,#106766,#106767,#106768,
#106769,#106770,#106771,#106772,#106773,#106774,#106775,#106776,#106777),
 .UNSPECIFIED.,.F.,.F.,(4,3,3,3,3,3,3,4),(26.2554830351793,26.7400349698051,
27.7304066353534,28.7207783009018,29.7111499664501,30.7015216319985,31.6918932975468,
32.5386683423589),.UNSPECIFIED.);
#24459=B_SPLINE_CURVE_WITH_KNOTS('',3,(#106782,#106783,#106784,#106785,
#106786,#106787,#106788,#106789,#106790,#106791,#106792,#106793,#106794,
#106795,#106796,#106797,#106798,#106799,#106800,#106801,#106802,#106803,
#106804,#106805,#106806),.UNSPECIFIED.,.F.,.F.,(4,3,3,3,3,3,3,3,4),(-41.7911353635261,
-41.5956099530302,-40.6052382874819,-39.6148666219335,-38.6244949563852,
-37.6341232908368,-36.6437516252885,-35.6533799597402,-35.5079500563465),
 .UNSPECIFIED.);
#24460=B_SPLINE_CURVE_WITH_KNOTS('',3,(#106807,#106808,#106809,#106810,
#106811,#106812,#106813,#106814,#106815,#106816,#106817,#106818,#106819,
#106820,#106821,#106822,#106823,#106824,#106825,#106826,#106827,#106828,
#106829,#106830,#106831),.UNSPECIFIED.,.F.,.F.,(4,3,3,3,3,3,3,3,4),(32.5386683423589,
32.6822649630951,33.6726366286435,34.6630082941918,35.6533799597401,36.6437516252885,
37.6341232908368,38.6244949563852,38.8218536495385),.UNSPECIFIED.);
#24461=B_SPLINE_CURVE_WITH_KNOTS('',3,(#106836,#106837,#106838,#106839,
#106840,#106841,#106842,#106843,#106844,#106845,#106846,#106847,#106848,
#106849,#106850,#106851,#106852,#106853,#106854,#106855,#106856,#106857),
 .UNSPECIFIED.,.F.,.F.,(4,3,3,3,3,3,3,4),(-48.0743206707057,-47.5378399463202,
-46.5474682807719,-45.5570966152235,-44.5667249496752,-43.5763532841269,
-42.5859816185785,-41.7911353635261),.UNSPECIFIED.);
#24462=B_SPLINE_CURVE_WITH_KNOTS('',3,(#106858,#106859,#106860,#106861,
#106862,#106863,#106864,#106865,#106866,#106867,#106868,#106869,#106870,
#106871,#106872,#106873,#106874,#106875,#106876,#106877,#106878,#106879),
 .UNSPECIFIED.,.F.,.F.,(4,3,3,3,3,3,3,4),(38.8218536495385,39.6148666219335,
40.6052382874818,41.5956099530302,42.5859816185785,43.5763532841269,44.5667249496752,
45.1050389567181),.UNSPECIFIED.);
#24463=B_SPLINE_CURVE_WITH_KNOTS('',3,(#106884,#106885,#106886,#106887,
#106888,#106889,#106890,#106891,#106892,#106893,#106894,#106895,#106896,
#106897,#106898,#106899,#106900,#106901,#106902,#106903,#106904,#106905),
 .UNSPECIFIED.,.F.,.F.,(4,3,3,3,3,3,3,4),(-54.3575059778853,-53.4800699396103,
-52.4896982740619,-51.4993266085136,-50.5089549429652,-49.5185832774169,
-48.5282116118686,-48.0743206707057),.UNSPECIFIED.);
#24464=B_SPLINE_CURVE_WITH_KNOTS('',3,(#106906,#106907,#106908,#106909,
#106910,#106911,#106912,#106913,#106914,#106915,#106916,#106917,#106918,
#106919,#106920,#106921,#106922,#106923,#106924,#106925,#106926,#106927),
 .UNSPECIFIED.,.F.,.F.,(4,3,3,3,3,3,3,4),(45.1050389567181,45.5570966152235,
46.5474682807719,47.5378399463202,48.5282116118685,49.5185832774169,50.5089549429652,
51.3882242638976),.UNSPECIFIED.);
#24465=B_SPLINE_CURVE_WITH_KNOTS('',3,(#106932,#106933,#106934,#106935,
#106936,#106937,#106938,#106939,#106940,#106941,#106942,#106943,#106944,
#106945,#106946,#106947,#106948,#106949,#106950,#106951,#106952,#106953,
#106954,#106955,#106956),.UNSPECIFIED.,.F.,.F.,(4,3,3,3,3,3,3,3,4),(-60.6406912850649,
-60.4126715984486,-59.4222999329003,-58.4319282673519,-57.4415566018036,
-56.4511849362553,-55.4608132707069,-54.4704416051586,-54.3575059778853),
 .UNSPECIFIED.);
#24466=B_SPLINE_CURVE_WITH_KNOTS('',3,(#106957,#106958,#106959,#106960,
#106961,#106962,#106963,#106964,#106965,#106966,#106967,#106968,#106969,
#106970,#106971,#106972,#106973,#106974,#106975,#106976,#106977,#106978,
#106979,#106980,#106981),.UNSPECIFIED.,.F.,.F.,(4,3,3,3,3,3,3,3,4),(51.3882242638976,
51.4993266085136,52.4896982740619,53.4800699396102,54.4704416051586,55.4608132707069,
56.4511849362552,57.4415566018036,57.6714095710772),.UNSPECIFIED.);
#24467=B_SPLINE_CURVE_WITH_KNOTS('',3,(#106986,#106987,#106988,#106989,
#106990,#106991,#106992,#106993,#106994,#106995,#106996,#106997,#106998,
#106999,#107000,#107001,#107002,#107003,#107004,#107005,#107006,#107007),
 .UNSPECIFIED.,.F.,.F.,(4,3,3,3,3,3,3,4),(-66.9238765922444,-66.3549015917386,
-65.3645299261903,-64.374158260642,-63.3837865950936,-62.3934149295453,
-61.403043263997,-60.6406912850649),.UNSPECIFIED.);
#24468=B_SPLINE_CURVE_WITH_KNOTS('',3,(#107008,#107009,#107010,#107011,
#107012,#107013,#107014,#107015,#107016,#107017,#107018,#107019,#107020,
#107021,#107022,#107023,#107024,#107025,#107026,#107027,#107028,#107029),
 .UNSPECIFIED.,.F.,.F.,(4,3,3,3,3,3,3,4),(57.6714095710772,58.4319282673519,
59.4222999329003,60.4126715984486,61.4030432639969,62.3934149295453,63.3837865950936,
63.9545948782568),.UNSPECIFIED.);
#24469=B_SPLINE_CURVE_WITH_KNOTS('',3,(#107035,#107036,#107037,#107038,
#107039,#107040,#107041,#107042,#107043),.UNSPECIFIED.,.F.,.F.,(4,1,1,1,
1,1,4),(72.2566310325652,73.0189830114973,74.0093546770456,74.999726342594,
75.9900980081423,76.9804696736907,77.878411997016),.UNSPECIFIED.);
#24470=B_SPLINE_CURVE_WITH_KNOTS('',3,(#107046,#107047,#107048,#107049,
#107050,#107051,#107052,#107053),.UNSPECIFIED.,.F.,.F.,(4,1,1,1,1,4),(72.2566310325652,
72.6761944149503,73.6665660804986,74.656937746047,75.6473094115953,76.6376810771436),
 .UNSPECIFIED.);
#24471=B_SPLINE_CURVE_WITH_KNOTS('',3,(#107058,#107059,#107060,#107061,
#107062,#107063,#107064,#107065,#107066,#107067,#107068),.UNSPECIFIED.,
 .F.,.F.,(4,1,1,1,1,1,1,1,4),(65.9734457253857,66.0863813526589,67.0767530182073,
68.0671246837556,69.057496349304,70.0478680148523,71.0382396804006,72.028611345949,
72.2566310325652),.UNSPECIFIED.);
#24472=B_SPLINE_CURVE_WITH_KNOTS('',3,(#107069,#107070,#107071,#107072,
#107073,#107074,#107075,#107076,#107077,#107078),.UNSPECIFIED.,.F.,.F.,
(4,1,1,1,1,1,1,4),(65.9734457253856,66.7339644216603,67.7243360872086,68.7147077527569,
69.7050794183053,70.6954510838536,71.685822749402,72.2566310325652),
 .UNSPECIFIED.);
#24473=B_SPLINE_CURVE_WITH_KNOTS('',3,(#107083,#107084,#107085,#107086,
#107087,#107088,#107089,#107090,#107091,#107092),.UNSPECIFIED.,.F.,.F.,
(4,1,1,1,1,1,1,4),(59.6902604182061,60.1441513593689,61.1345230249173,62.1248946904656,
63.1152663560139,64.1056380215623,65.0960096871106,65.9734457253857),
 .UNSPECIFIED.);
#24474=B_SPLINE_CURVE_WITH_KNOTS('',3,(#107093,#107094,#107095,#107096,
#107097,#107098,#107099,#107100,#107101,#107102,#107103),.UNSPECIFIED.,
 .F.,.F.,(4,1,1,1,1,1,1,1,4),(59.690260418206,59.8013627628219,60.7917344283702,
61.7821060939186,62.7724777594669,63.7628494250152,64.7532210905636,65.7435927561119,
65.9734457253856),.UNSPECIFIED.);
#24475=B_SPLINE_CURVE_WITH_KNOTS('',3,(#107108,#107109,#107110,#107111,
#107112,#107113,#107114,#107115,#107116,#107117),.UNSPECIFIED.,.F.,.F.,
(4,1,1,1,1,1,1,4),(53.4070751110265,54.2019213660789,55.1922930316272,56.1826646971756,
57.1730363627239,58.1634080282722,59.1537796938206,59.6902604182061),
 .UNSPECIFIED.);
#24476=B_SPLINE_CURVE_WITH_KNOTS('',3,(#107118,#107119,#107120,#107121,
#107122,#107123,#107124,#107125,#107126,#107127),.UNSPECIFIED.,.F.,.F.,
(4,1,1,1,1,1,1,4),(53.4070751110265,53.8591327695319,54.8495044350802,55.8398761006285,
56.8302477661769,57.8206194317252,58.8109910972736,59.690260418206),
 .UNSPECIFIED.);
#24477=B_SPLINE_CURVE_WITH_KNOTS('',3,(#107132,#107133,#107134,#107135,
#107136,#107137,#107138,#107139,#107140,#107141,#107142),.UNSPECIFIED.,
 .F.,.F.,(4,1,1,1,1,1,1,1,4),(47.1238898038469,47.2693197072405,48.2596913727889,
49.2500630383372,50.2404347038855,51.2308063694339,52.2211780349822,53.2115497005306,
53.4070751110265),.UNSPECIFIED.);
#24478=B_SPLINE_CURVE_WITH_KNOTS('',3,(#107143,#107144,#107145,#107146,
#107147,#107148,#107149,#107150,#107151,#107152),.UNSPECIFIED.,.F.,.F.,
(4,1,1,1,1,1,1,4),(47.1238898038469,47.9169027762418,48.9072744417902,49.8976461073385,
50.8880177728869,51.8783894384352,52.8687611039835,53.4070751110265),
 .UNSPECIFIED.);
#24479=B_SPLINE_CURVE_WITH_KNOTS('',3,(#107157,#107158,#107159,#107160,
#107161,#107162,#107163,#107164,#107165,#107166),.UNSPECIFIED.,.F.,.F.,
(4,1,1,1,1,1,1,4),(40.8407044966673,41.3270897139505,42.3174613794988,43.3078330450472,
44.2982047105955,45.2885763761439,46.2789480416922,47.1238898038469),
 .UNSPECIFIED.);
#24480=B_SPLINE_CURVE_WITH_KNOTS('',3,(#107167,#107168,#107169,#107170,
#107171,#107172,#107173,#107174,#107175,#107176,#107177),.UNSPECIFIED.,
 .F.,.F.,(4,1,1,1,1,1,1,1,4),(40.8407044966673,40.9843011174035,41.9746727829518,
42.9650444485002,43.9554161140485,44.9457877795968,45.9361594451452,46.9265311106935,
47.1238898038469),.UNSPECIFIED.);
#24481=B_SPLINE_CURVE_WITH_KNOTS('',3,(#107182,#107183,#107184,#107185,
#107186,#107187,#107188,#107189,#107190,#107191),.UNSPECIFIED.,.F.,.F.,
(4,1,1,1,1,1,1,4),(34.5575191894877,35.3848597206605,36.3752313862088,37.3656030517571,
38.3559747173055,39.3463463828538,40.3367180484022,40.8407044966673),
 .UNSPECIFIED.);
#24482=B_SPLINE_CURVE_WITH_KNOTS('',3,(#107192,#107193,#107194,#107195,
#107196,#107197,#107198,#107199,#107200,#107201),.UNSPECIFIED.,.F.,.F.,
(4,1,1,1,1,1,1,4),(34.5575191894877,35.0420711241134,36.0324427896618,37.0228144552101,
38.0131861207585,39.0035577863068,39.9939294518551,40.8407044966673),
 .UNSPECIFIED.);
#24483=B_SPLINE_CURVE_WITH_KNOTS('',3,(#107206,#107207,#107208,#107209,
#107210,#107211,#107212,#107213,#107214,#107215,#107216),.UNSPECIFIED.,
 .F.,.F.,(4,1,1,1,1,1,1,1,4),(28.2743338823081,28.4522580618221,29.4426297273704,
30.4330013929188,31.4233730584671,32.4137447240155,33.4041163895638,34.3944880551121,
34.5575191894877),.UNSPECIFIED.);
#24484=B_SPLINE_CURVE_WITH_KNOTS('',3,(#107217,#107218,#107219,#107220,
#107221,#107222,#107223,#107224,#107225,#107226),.UNSPECIFIED.,.F.,.F.,
(4,1,1,1,1,1,1,4),(28.2743338823081,29.0998411308234,30.0902127963718,31.0805844619201,
32.0709561274684,33.0613277930168,34.0516994585651,34.5575191894877),
 .UNSPECIFIED.);
#24485=B_SPLINE_CURVE_WITH_KNOTS('',3,(#107231,#107232,#107233,#107234,
#107235,#107236,#107237,#107238,#107239,#107240),.UNSPECIFIED.,.F.,.F.,
(4,1,1,1,1,1,1,4),(21.9911485751285,22.5100280685321,23.5003997340804,24.4907713996288,
25.4811430651771,26.4715147307254,27.4618863962738,28.2743338823081),
 .UNSPECIFIED.);
#24486=B_SPLINE_CURVE_WITH_KNOTS('',3,(#107241,#107242,#107243,#107244,
#107245,#107246,#107247,#107248,#107249,#107250,#107251),.UNSPECIFIED.,
 .F.,.F.,(4,1,1,1,1,1,1,1,4),(21.9911485751285,22.1672394719851,23.1576111375334,
24.1479828030817,25.1383544686301,26.1287261341784,27.1190977997268,28.1094694652751,
28.2743338823081),.UNSPECIFIED.);
#24487=B_SPLINE_CURVE_WITH_KNOTS('',3,(#107256,#107257,#107258,#107259,
#107260,#107261,#107262,#107263,#107264,#107265),.UNSPECIFIED.,.F.,.F.,
(4,1,1,1,1,1,1,4),(15.7079632679489,16.5677980752421,17.5581697407904,18.5485414063387,
19.5389130718871,20.5292847374354,21.5196564029837,21.9911485751285),
 .UNSPECIFIED.);
#24488=B_SPLINE_CURVE_WITH_KNOTS('',3,(#107266,#107267,#107268,#107269,
#107270,#107271,#107272,#107273,#107274,#107275),.UNSPECIFIED.,.F.,.F.,
(4,1,1,1,1,1,1,4),(15.7079632679489,16.225009478695,17.2153811442434,18.2057528097917,
19.19612447534,20.1864961408884,21.1768678064367,21.9911485751285),
 .UNSPECIFIED.);
#24489=B_SPLINE_CURVE_WITH_KNOTS('',3,(#107278,#107279,#107280,#107281,
#107282,#107283,#107284,#107285,#107286,#107287,#107288,#107289,#107290,
#107291,#107292,#107293,#107294,#107295,#107296,#107297,#107298,#107299,
#107300,#107301,#107302,#107303,#107304,#107305,#107306,#107307,#107308,
#107309,#107310,#107311,#107312,#107313,#107314,#107315,#107316,#107317,
#107318,#107319,#107320,#107321,#107322,#107323,#107324,#107325,#107326,
#107327,#107328,#107329,#107330,#107331,#107332,#107333,#107334,#107335,
#107336,#107337,#107338,#107339,#107340,#107341,#107342,#107343,#107344,
#107345,#107346,#107347,#107348,#107349,#107350,#107351,#107352,#107353,
#107354,#107355,#107356,#107357,#107358,#107359,#107360,#107361,#107362),
 .UNSPECIFIED.,.F.,.F.,(4,3,3,3,3,3,3,3,3,3,3,3,3,3,3,3,3,3,3,3,3,3,3,3,
3,3,3,3,4),(-0.276631791712726,-0.265556404172054,-0.250893761334244,-0.246326614508792,
-0.242071276684929,-0.226809496625315,-0.215889342634413,-0.212053933697475,
-0.209215860671437,-0.193472099741198,-0.177422787794644,-0.167929157020507,
-0.163043036473233,-0.159563271570797,-0.143037655072155,-0.139448264698093,
-0.123479171928492,-0.115761723682961,-0.11087518000946,-0.107810715979693,
-0.0912632113418131,-0.0743540660658942,-0.0648503094985542,-0.0586274039788276,
-0.0554898421713441,-0.038048405855375,-0.0205610872293301,-0.00347583643527304,
0.),.UNSPECIFIED.);
#24490=B_SPLINE_CURVE_WITH_KNOTS('',3,(#107367,#107368,#107369,#107370,
#107371,#107372,#107373,#107374,#107375,#107376,#107377,#107378,#107379,
#107380,#107381,#107382,#107383,#107384,#107385,#107386,#107387,#107388,
#107389,#107390,#107391,#107392,#107393,#107394,#107395,#107396,#107397,
#107398,#107399,#107400,#107401,#107402,#107403,#107404,#107405,#107406,
#107407,#107408,#107409,#107410,#107411,#107412,#107413,#107414,#107415,
#107416,#107417,#107418,#107419,#107420,#107421,#107422,#107423,#107424,
#107425,#107426,#107427,#107428,#107429,#107430,#107431,#107432,#107433,
#107434,#107435,#107436,#107437,#107438,#107439,#107440,#107441,#107442,
#107443,#107444,#107445,#107446,#107447,#107448),.UNSPECIFIED.,.F.,.F.,
(4,3,3,3,3,3,3,3,3,3,3,3,3,3,3,3,3,3,3,3,3,3,3,3,3,3,3,4),(-0.275362278356893,
-0.261872343204998,-0.24468860577658,-0.238154470087611,-0.234296428116099,
-0.217100289999107,-0.205513059221426,-0.20049709699629,-0.197078549988272,
-0.180325629008319,-0.163976579024965,-0.154083045213138,-0.146647746749225,
-0.143758439830075,-0.127907386038086,-0.124402443777657,-0.107856521591035,
-0.100778967419367,-0.0955723543570963,-0.09258481164279,-0.0768191855824136,
-0.0611312890502507,-0.053290039364698,-0.0475073352526531,-0.0447090506925457,
-0.029602296160261,-0.0148011480801305,0.),.UNSPECIFIED.);
#24491=B_SPLINE_CURVE_WITH_KNOTS('',3,(#107737,#107738,#107739,#107740,
#107741,#107742,#107743,#107744,#107745,#107746),.UNSPECIFIED.,.F.,.F.,
(4,3,3,4),(63.9545948782568,64.374158260642,65.3645299261903,66.2624722495156),
 .UNSPECIFIED.);
#24492=B_SPLINE_CURVE_WITH_KNOTS('',3,(#107748,#107749,#107750,#107751,
#107752,#107753,#107754,#107755,#107756,#107757,#107758,#107759,#107760,
#107761,#107762,#107763,#107764,#107765,#107766,#107767,#107768,#107769,
#107770,#107771,#107772,#107773,#107774,#107775,#107776,#107777,#107778,
#107779,#107780,#107781,#107782,#107783,#107784,#107785,#107786,#107787,
#107788,#107789,#107790,#107791,#107792,#107793,#107794,#107795,#107796,
#107797,#107798,#107799,#107800,#107801,#107802,#107803,#107804,#107805,
#107806,#107807,#107808,#107809,#107810,#107811,#107812,#107813,#107814,
#107815,#107816,#107817,#107818,#107819,#107820,#107821,#107822,#107823,
#107824,#107825,#107826,#107827,#107828,#107829,#107830,#107831,#107832),
 .UNSPECIFIED.,.F.,.F.,(4,3,3,3,3,3,3,3,3,3,3,3,3,3,3,3,3,3,3,3,3,3,3,3,
3,3,3,3,4),(-0.276631791712751,-0.265556404172093,-0.250893754106259,-0.246326629283502,
-0.242071279945798,-0.22680949525836,-0.215889341438329,-0.212053930423597,
-0.209215853958591,-0.193472089270526,-0.177422778058093,-0.167929149718099,
-0.163043027431145,-0.159563268993254,-0.143037653194888,-0.139448264698117,
-0.123479168511542,-0.11576172047957,-0.110875178909016,-0.10781071624844,
-0.0912632076335315,-0.0743540586873285,-0.0648503081023367,-0.0586274009532849,
-0.0554898388596249,-0.0380483998101587,-0.0205610837999868,-0.00347584549412929,
0.),.UNSPECIFIED.);
#24493=B_SPLINE_CURVE_WITH_KNOTS('',3,(#107833,#107834,#107835,#107836,
#107837,#107838,#107839,#107840,#107841),.UNSPECIFIED.,.F.,.F.,(4,1,1,1,
1,1,4),(10.375208827628,11.2731511509533,12.2635228165017,13.25389448205,
14.2442661475984,15.2346378131467,15.7079632679489),.UNSPECIFIED.);
#24494=B_SPLINE_CURVE_WITH_KNOTS('',3,(#107847,#107848,#107849,#107850,
#107851,#107852,#107853,#107854,#107855,#107856,#107857,#107858,#107859,
#107860,#107861,#107862,#107863,#107864,#107865,#107866,#107867,#107868,
#107869,#107870,#107871,#107872,#107873,#107874,#107875,#107876,#107877,
#107878,#107879,#107880,#107881,#107882,#107883,#107884,#107885,#107886,
#107887,#107888,#107889,#107890,#107891,#107892,#107893,#107894,#107895,
#107896,#107897,#107898,#107899,#107900,#107901,#107902,#107903,#107904,
#107905,#107906,#107907,#107908,#107909,#107910,#107911,#107912,#107913,
#107914,#107915,#107916,#107917,#107918,#107919,#107920,#107921,#107922,
#107923,#107924,#107925,#107926,#107927,#107928),.UNSPECIFIED.,.F.,.F.,
(4,3,3,3,3,3,3,3,3,3,3,3,3,3,3,3,3,3,3,3,3,3,3,3,3,3,3,4),(-0.275362278356958,
-0.261872343205071,-0.244688605776648,-0.238154479469242,-0.234296429189573,
-0.217100291206748,-0.205513060278116,-0.200497101796343,-0.197078550198523,
-0.180325630119186,-0.163976587765092,-0.154083051768242,-0.14664777167162,
-0.143758474849684,-0.127907428224212,-0.124402443777692,-0.107856504661946,
-0.100778964786935,-0.0955723501300554,-0.0925848098741145,-0.0768191852239964,
-0.0611312820723457,-0.053290036945375,-0.047507330004606,-0.0447090458564731,
-0.0296022827355091,-0.0148011413677545,0.),.UNSPECIFIED.);
#24495=B_SPLINE_CURVE_WITH_KNOTS('',3,(#107931,#107932,#107933,#107934,
#107935,#107936,#107937,#107938),.UNSPECIFIED.,.F.,.F.,(4,1,1,1,1,4),(11.6159397475004,
12.6063114130487,13.596683078597,14.5870547441454,15.5774264096937,15.7079632679489),
 .UNSPECIFIED.);
#24496=B_SPLINE_CURVE_WITH_KNOTS('',3,(#108227,#108228,#108229,#108230,
#108231,#108232,#108233),.UNSPECIFIED.,.F.,.F.,(4,3,4),(-68.3356449228353,
-67.345273257287,-66.9238765922444),.UNSPECIFIED.);
#29808=VERTEX_POINT('',#106509);
#29809=VERTEX_POINT('',#106510);
#29810=VERTEX_POINT('',#106512);
#29811=VERTEX_POINT('',#106523);
#29812=VERTEX_POINT('',#106533);
#29813=VERTEX_POINT('',#106534);
#29814=VERTEX_POINT('',#106581);
#29815=VERTEX_POINT('',#106582);
#29816=VERTEX_POINT('',#106629);
#29817=VERTEX_POINT('',#106630);
#29818=VERTEX_POINT('',#106683);
#29819=VERTEX_POINT('',#106684);
#29820=VERTEX_POINT('',#106731);
#29821=VERTEX_POINT('',#106732);
#29822=VERTEX_POINT('',#106779);
#29823=VERTEX_POINT('',#106780);
#29824=VERTEX_POINT('',#106833);
#29825=VERTEX_POINT('',#106834);
#29826=VERTEX_POINT('',#106881);
#29827=VERTEX_POINT('',#106882);
#29828=VERTEX_POINT('',#106929);
#29829=VERTEX_POINT('',#106930);
#29830=VERTEX_POINT('',#106983);
#29831=VERTEX_POINT('',#106984);
#29832=VERTEX_POINT('',#107031);
#29833=VERTEX_POINT('',#107032);
#29834=VERTEX_POINT('',#107034);
#29835=VERTEX_POINT('',#107044);
#29836=VERTEX_POINT('',#107055);
#29837=VERTEX_POINT('',#107056);
#29838=VERTEX_POINT('',#107080);
#29839=VERTEX_POINT('',#107081);
#29840=VERTEX_POINT('',#107105);
#29841=VERTEX_POINT('',#107106);
#29842=VERTEX_POINT('',#107129);
#29843=VERTEX_POINT('',#107130);
#29844=VERTEX_POINT('',#107154);
#29845=VERTEX_POINT('',#107155);
#29846=VERTEX_POINT('',#107179);
#29847=VERTEX_POINT('',#107180);
#29848=VERTEX_POINT('',#107203);
#29849=VERTEX_POINT('',#107204);
#29850=VERTEX_POINT('',#107228);
#29851=VERTEX_POINT('',#107229);
#29852=VERTEX_POINT('',#107253);
#29853=VERTEX_POINT('',#107254);
#29854=VERTEX_POINT('',#107277);
#29855=VERTEX_POINT('',#107363);
#29856=VERTEX_POINT('',#107365);
#29857=VERTEX_POINT('',#107747);
#29858=VERTEX_POINT('',#107843);
#29859=VERTEX_POINT('',#107846);
#29860=VERTEX_POINT('',#108235);
#29861=VERTEX_POINT('',#108237);
#29862=VERTEX_POINT('',#108239);
#29863=VERTEX_POINT('',#108243);
#29864=VERTEX_POINT('',#108245);
#29865=VERTEX_POINT('',#108249);
#29866=VERTEX_POINT('',#108253);
#29867=VERTEX_POINT('',#108255);
#29868=VERTEX_POINT('',#108259);
#29869=VERTEX_POINT('',#108263);
#29870=VERTEX_POINT('',#108265);
#29871=VERTEX_POINT('',#108269);
#29872=VERTEX_POINT('',#108273);
#29873=VERTEX_POINT('',#108275);
#29874=VERTEX_POINT('',#108279);
#29875=VERTEX_POINT('',#108283);
#29876=VERTEX_POINT('',#108285);
#29877=VERTEX_POINT('',#108289);
#29878=VERTEX_POINT('',#108293);
#29879=VERTEX_POINT('',#108299);
#29880=VERTEX_POINT('',#108301);
#29881=VERTEX_POINT('',#108305);
#29882=VERTEX_POINT('',#108307);
#29883=VERTEX_POINT('',#108311);
#29884=VERTEX_POINT('',#108313);
#29885=VERTEX_POINT('',#108317);
#29886=VERTEX_POINT('',#108319);
#29887=VERTEX_POINT('',#108323);
#29888=VERTEX_POINT('',#108325);
#29889=VERTEX_POINT('',#108329);
#29890=VERTEX_POINT('',#108331);
#29891=VERTEX_POINT('',#108336);
#29892=VERTEX_POINT('',#108338);
#29893=VERTEX_POINT('',#108343);
#29894=VERTEX_POINT('',#108348);
#29895=VERTEX_POINT('',#108361);
#29896=VERTEX_POINT('',#108371);
#29897=VERTEX_POINT('',#108378);
#29898=VERTEX_POINT('',#108386);
#29899=VERTEX_POINT('',#108393);
#38195=EDGE_CURVE('',#29808,#29809,#16531,.T.);
#38196=EDGE_CURVE('',#29808,#29810,#24447,.T.);
#38197=EDGE_CURVE('',#29810,#29811,#1361,.T.);
#38198=EDGE_CURVE('',#29811,#29809,#24448,.T.);
#38199=EDGE_CURVE('',#29812,#29813,#16532,.T.);
#38200=EDGE_CURVE('',#29812,#29808,#24449,.T.);
#38201=EDGE_CURVE('',#29809,#29813,#24450,.T.);
#38202=EDGE_CURVE('',#29814,#29815,#16533,.T.);
#38203=EDGE_CURVE('',#29814,#29812,#24451,.T.);
#38204=EDGE_CURVE('',#29813,#29815,#24452,.T.);
#38205=EDGE_CURVE('',#29816,#29817,#16534,.T.);
#38206=EDGE_CURVE('',#29816,#29814,#24453,.T.);
#38207=EDGE_CURVE('',#29815,#29817,#24454,.T.);
#38208=EDGE_CURVE('',#29818,#29819,#16535,.T.);
#38209=EDGE_CURVE('',#29818,#29816,#24455,.T.);
#38210=EDGE_CURVE('',#29817,#29819,#24456,.T.);
#38211=EDGE_CURVE('',#29820,#29821,#16536,.T.);
#38212=EDGE_CURVE('',#29820,#29818,#24457,.T.);
#38213=EDGE_CURVE('',#29819,#29821,#24458,.T.);
#38214=EDGE_CURVE('',#29822,#29823,#16537,.T.);
#38215=EDGE_CURVE('',#29822,#29820,#24459,.T.);
#38216=EDGE_CURVE('',#29821,#29823,#24460,.T.);
#38217=EDGE_CURVE('',#29824,#29825,#16538,.T.);
#38218=EDGE_CURVE('',#29824,#29822,#24461,.T.);
#38219=EDGE_CURVE('',#29823,#29825,#24462,.T.);
#38220=EDGE_CURVE('',#29826,#29827,#16539,.T.);
#38221=EDGE_CURVE('',#29826,#29824,#24463,.T.);
#38222=EDGE_CURVE('',#29825,#29827,#24464,.T.);
#38223=EDGE_CURVE('',#29828,#29829,#16540,.T.);
#38224=EDGE_CURVE('',#29828,#29826,#24465,.T.);
#38225=EDGE_CURVE('',#29827,#29829,#24466,.T.);
#38226=EDGE_CURVE('',#29830,#29831,#16541,.T.);
#38227=EDGE_CURVE('',#29830,#29828,#24467,.T.);
#38228=EDGE_CURVE('',#29829,#29831,#24468,.T.);
#38229=EDGE_CURVE('',#29832,#29833,#16542,.T.);
#38230=EDGE_CURVE('',#29832,#29834,#24469,.T.);
#38231=EDGE_CURVE('',#29835,#29834,#1362,.T.);
#38232=EDGE_CURVE('',#29833,#29835,#24470,.T.);
#38233=EDGE_CURVE('',#29836,#29837,#16543,.T.);
#38234=EDGE_CURVE('',#29836,#29832,#24471,.T.);
#38235=EDGE_CURVE('',#29837,#29833,#24472,.T.);
#38236=EDGE_CURVE('',#29838,#29839,#16544,.T.);
#38237=EDGE_CURVE('',#29838,#29836,#24473,.T.);
#38238=EDGE_CURVE('',#29839,#29837,#24474,.T.);
#38239=EDGE_CURVE('',#29840,#29841,#16545,.T.);
#38240=EDGE_CURVE('',#29840,#29838,#24475,.T.);
#38241=EDGE_CURVE('',#29841,#29839,#24476,.T.);
#38242=EDGE_CURVE('',#29842,#29843,#16546,.T.);
#38243=EDGE_CURVE('',#29842,#29840,#24477,.T.);
#38244=EDGE_CURVE('',#29843,#29841,#24478,.T.);
#38245=EDGE_CURVE('',#29844,#29845,#16547,.T.);
#38246=EDGE_CURVE('',#29844,#29842,#24479,.T.);
#38247=EDGE_CURVE('',#29845,#29843,#24480,.T.);
#38248=EDGE_CURVE('',#29846,#29847,#16548,.T.);
#38249=EDGE_CURVE('',#29846,#29844,#24481,.T.);
#38250=EDGE_CURVE('',#29847,#29845,#24482,.T.);
#38251=EDGE_CURVE('',#29848,#29849,#16549,.T.);
#38252=EDGE_CURVE('',#29848,#29846,#24483,.T.);
#38253=EDGE_CURVE('',#29849,#29847,#24484,.T.);
#38254=EDGE_CURVE('',#29850,#29851,#16550,.T.);
#38255=EDGE_CURVE('',#29850,#29848,#24485,.T.);
#38256=EDGE_CURVE('',#29851,#29849,#24486,.T.);
#38257=EDGE_CURVE('',#29852,#29853,#16551,.T.);
#38258=EDGE_CURVE('',#29852,#29850,#24487,.T.);
#38259=EDGE_CURVE('',#29853,#29851,#24488,.T.);
#38260=EDGE_CURVE('',#29834,#29854,#24489,.T.);
#38261=EDGE_CURVE('',#29855,#29854,#1363,.F.);
#38262=EDGE_CURVE('',#29856,#29855,#1364,.F.);
#38263=EDGE_CURVE('',#29856,#29835,#24490,.T.);
#38264=EDGE_CURVE('',#29831,#29856,#24491,.T.);
#38265=EDGE_CURVE('',#29857,#29811,#24492,.T.);
#38266=EDGE_CURVE('',#29857,#29853,#24493,.T.);
#38267=EDGE_CURVE('',#29811,#29858,#1365,.T.);
#38268=EDGE_CURVE('',#29858,#29810,#1366,.T.);
#38269=EDGE_CURVE('',#29810,#29859,#24494,.T.);
#38270=EDGE_CURVE('',#29859,#29857,#1367,.T.);
#38271=EDGE_CURVE('',#29859,#29852,#24495,.T.);
#38272=EDGE_CURVE('',#29854,#29830,#24496,.T.);
#38273=EDGE_CURVE('',#29860,#29860,#1368,.T.);
#38274=EDGE_CURVE('',#29860,#29861,#16552,.T.);
#38275=EDGE_CURVE('',#29862,#29861,#407,.T.);
#38276=EDGE_CURVE('',#29862,#29863,#1369,.T.);
#38277=EDGE_CURVE('',#29864,#29863,#408,.T.);
#38278=EDGE_CURVE('',#29865,#29864,#409,.T.);
#38279=EDGE_CURVE('',#29865,#29866,#1370,.T.);
#38280=EDGE_CURVE('',#29867,#29866,#410,.T.);
#38281=EDGE_CURVE('',#29868,#29867,#411,.T.);
#38282=EDGE_CURVE('',#29868,#29869,#1371,.T.);
#38283=EDGE_CURVE('',#29870,#29869,#412,.T.);
#38284=EDGE_CURVE('',#29871,#29870,#413,.T.);
#38285=EDGE_CURVE('',#29871,#29872,#1372,.T.);
#38286=EDGE_CURVE('',#29873,#29872,#414,.T.);
#38287=EDGE_CURVE('',#29874,#29873,#415,.T.);
#38288=EDGE_CURVE('',#29874,#29875,#1373,.T.);
#38289=EDGE_CURVE('',#29876,#29875,#416,.T.);
#38290=EDGE_CURVE('',#29877,#29876,#417,.T.);
#38291=EDGE_CURVE('',#29877,#29878,#1374,.T.);
#38292=EDGE_CURVE('',#29861,#29878,#418,.T.);
#38293=EDGE_CURVE('',#29869,#29879,#16553,.T.);
#38294=EDGE_CURVE('',#29880,#29868,#16554,.T.);
#38295=EDGE_CURVE('',#29879,#29880,#1375,.T.);
#38296=EDGE_CURVE('',#29872,#29881,#16555,.T.);
#38297=EDGE_CURVE('',#29882,#29871,#16556,.T.);
#38298=EDGE_CURVE('',#29881,#29882,#1376,.T.);
#38299=EDGE_CURVE('',#29883,#29865,#16557,.T.);
#38300=EDGE_CURVE('',#29884,#29883,#1377,.T.);
#38301=EDGE_CURVE('',#29866,#29884,#16558,.T.);
#38302=EDGE_CURVE('',#29875,#29885,#16559,.T.);
#38303=EDGE_CURVE('',#29886,#29874,#16560,.T.);
#38304=EDGE_CURVE('',#29885,#29886,#1378,.T.);
#38305=EDGE_CURVE('',#29887,#29862,#16561,.T.);
#38306=EDGE_CURVE('',#29888,#29887,#1379,.T.);
#38307=EDGE_CURVE('',#29863,#29888,#16562,.T.);
#38308=EDGE_CURVE('',#29889,#29877,#16563,.T.);
#38309=EDGE_CURVE('',#29890,#29889,#1380,.T.);
#38310=EDGE_CURVE('',#29878,#29890,#16564,.T.);
#38311=EDGE_CURVE('',#29886,#29885,#16565,.T.);
#38312=EDGE_CURVE('',#29873,#29891,#16566,.T.);
#38313=EDGE_CURVE('',#29891,#29892,#16567,.T.);
#38314=EDGE_CURVE('',#29876,#29892,#16568,.T.);
#38315=EDGE_CURVE('',#29882,#29881,#16569,.T.);
#38316=EDGE_CURVE('',#29870,#29893,#16570,.T.);
#38317=EDGE_CURVE('',#29893,#29891,#16571,.T.);
#38318=EDGE_CURVE('',#29880,#29879,#16572,.T.);
#38319=EDGE_CURVE('',#29867,#29894,#16573,.T.);
#38320=EDGE_CURVE('',#29894,#29893,#16574,.T.);
#38321=EDGE_CURVE('',#29883,#29884,#16575,.T.);
#38322=EDGE_CURVE('',#29887,#29888,#16576,.T.);
#38323=EDGE_CURVE('',#29889,#29890,#16577,.T.);
#38324=EDGE_CURVE('',#29895,#29894,#16578,.T.);
#38325=EDGE_CURVE('',#29895,#29894,#1381,.T.);
#38326=EDGE_CURVE('',#29894,#29893,#1382,.T.);
#38327=EDGE_CURVE('',#29893,#29891,#1383,.T.);
#38328=EDGE_CURVE('',#29891,#29892,#1384,.T.);
#38329=EDGE_CURVE('',#29892,#29896,#16579,.T.);
#38330=EDGE_CURVE('',#29892,#29896,#1385,.T.);
#38331=EDGE_CURVE('',#29896,#29895,#16580,.T.);
#38332=EDGE_CURVE('',#29896,#29895,#1386,.T.);
#38333=EDGE_CURVE('',#29896,#29897,#16581,.T.);
#38334=EDGE_CURVE('',#29864,#29895,#16582,.T.);
#38335=EDGE_CURVE('',#29861,#29896,#16583,.T.);
#38336=EDGE_CURVE('',#29898,#29898,#1387,.T.);
#38337=EDGE_CURVE('',#29858,#29898,#16584,.T.);
#38338=EDGE_CURVE('',#29854,#29856,#1388,.F.);
#38339=EDGE_CURVE('',#29899,#29899,#1389,.T.);
#38340=EDGE_CURVE('',#29899,#29855,#16585,.T.);
#54725=ORIENTED_EDGE('',*,*,#38195,.F.);
#54726=ORIENTED_EDGE('',*,*,#38196,.T.);
#54727=ORIENTED_EDGE('',*,*,#38197,.T.);
#54728=ORIENTED_EDGE('',*,*,#38198,.T.);
#54729=ORIENTED_EDGE('',*,*,#38199,.F.);
#54730=ORIENTED_EDGE('',*,*,#38200,.T.);
#54731=ORIENTED_EDGE('',*,*,#38195,.T.);
#54732=ORIENTED_EDGE('',*,*,#38201,.T.);
#54733=ORIENTED_EDGE('',*,*,#38202,.F.);
#54734=ORIENTED_EDGE('',*,*,#38203,.T.);
#54735=ORIENTED_EDGE('',*,*,#38199,.T.);
#54736=ORIENTED_EDGE('',*,*,#38204,.T.);
#54737=ORIENTED_EDGE('',*,*,#38205,.F.);
#54738=ORIENTED_EDGE('',*,*,#38206,.T.);
#54739=ORIENTED_EDGE('',*,*,#38202,.T.);
#54740=ORIENTED_EDGE('',*,*,#38207,.T.);
#54741=ORIENTED_EDGE('',*,*,#38208,.F.);
#54742=ORIENTED_EDGE('',*,*,#38209,.T.);
#54743=ORIENTED_EDGE('',*,*,#38205,.T.);
#54744=ORIENTED_EDGE('',*,*,#38210,.T.);
#54745=ORIENTED_EDGE('',*,*,#38211,.F.);
#54746=ORIENTED_EDGE('',*,*,#38212,.T.);
#54747=ORIENTED_EDGE('',*,*,#38208,.T.);
#54748=ORIENTED_EDGE('',*,*,#38213,.T.);
#54749=ORIENTED_EDGE('',*,*,#38214,.F.);
#54750=ORIENTED_EDGE('',*,*,#38215,.T.);
#54751=ORIENTED_EDGE('',*,*,#38211,.T.);
#54752=ORIENTED_EDGE('',*,*,#38216,.T.);
#54753=ORIENTED_EDGE('',*,*,#38217,.F.);
#54754=ORIENTED_EDGE('',*,*,#38218,.T.);
#54755=ORIENTED_EDGE('',*,*,#38214,.T.);
#54756=ORIENTED_EDGE('',*,*,#38219,.T.);
#54757=ORIENTED_EDGE('',*,*,#38220,.F.);
#54758=ORIENTED_EDGE('',*,*,#38221,.T.);
#54759=ORIENTED_EDGE('',*,*,#38217,.T.);
#54760=ORIENTED_EDGE('',*,*,#38222,.T.);
#54761=ORIENTED_EDGE('',*,*,#38223,.F.);
#54762=ORIENTED_EDGE('',*,*,#38224,.T.);
#54763=ORIENTED_EDGE('',*,*,#38220,.T.);
#54764=ORIENTED_EDGE('',*,*,#38225,.T.);
#54765=ORIENTED_EDGE('',*,*,#38226,.F.);
#54766=ORIENTED_EDGE('',*,*,#38227,.T.);
#54767=ORIENTED_EDGE('',*,*,#38223,.T.);
#54768=ORIENTED_EDGE('',*,*,#38228,.T.);
#54769=ORIENTED_EDGE('',*,*,#38229,.F.);
#54770=ORIENTED_EDGE('',*,*,#38230,.T.);
#54771=ORIENTED_EDGE('',*,*,#38231,.F.);
#54772=ORIENTED_EDGE('',*,*,#38232,.F.);
#54773=ORIENTED_EDGE('',*,*,#38233,.F.);
#54774=ORIENTED_EDGE('',*,*,#38234,.T.);
#54775=ORIENTED_EDGE('',*,*,#38229,.T.);
#54776=ORIENTED_EDGE('',*,*,#38235,.F.);
#54777=ORIENTED_EDGE('',*,*,#38236,.F.);
#54778=ORIENTED_EDGE('',*,*,#38237,.T.);
#54779=ORIENTED_EDGE('',*,*,#38233,.T.);
#54780=ORIENTED_EDGE('',*,*,#38238,.F.);
#54781=ORIENTED_EDGE('',*,*,#38239,.F.);
#54782=ORIENTED_EDGE('',*,*,#38240,.T.);
#54783=ORIENTED_EDGE('',*,*,#38236,.T.);
#54784=ORIENTED_EDGE('',*,*,#38241,.F.);
#54785=ORIENTED_EDGE('',*,*,#38242,.F.);
#54786=ORIENTED_EDGE('',*,*,#38243,.T.);
#54787=ORIENTED_EDGE('',*,*,#38239,.T.);
#54788=ORIENTED_EDGE('',*,*,#38244,.F.);
#54789=ORIENTED_EDGE('',*,*,#38245,.F.);
#54790=ORIENTED_EDGE('',*,*,#38246,.T.);
#54791=ORIENTED_EDGE('',*,*,#38242,.T.);
#54792=ORIENTED_EDGE('',*,*,#38247,.F.);
#54793=ORIENTED_EDGE('',*,*,#38248,.F.);
#54794=ORIENTED_EDGE('',*,*,#38249,.T.);
#54795=ORIENTED_EDGE('',*,*,#38245,.T.);
#54796=ORIENTED_EDGE('',*,*,#38250,.F.);
#54797=ORIENTED_EDGE('',*,*,#38251,.F.);
#54798=ORIENTED_EDGE('',*,*,#38252,.T.);
#54799=ORIENTED_EDGE('',*,*,#38248,.T.);
#54800=ORIENTED_EDGE('',*,*,#38253,.F.);
#54801=ORIENTED_EDGE('',*,*,#38254,.F.);
#54802=ORIENTED_EDGE('',*,*,#38255,.T.);
#54803=ORIENTED_EDGE('',*,*,#38251,.T.);
#54804=ORIENTED_EDGE('',*,*,#38256,.F.);
#54805=ORIENTED_EDGE('',*,*,#38257,.F.);
#54806=ORIENTED_EDGE('',*,*,#38258,.T.);
#54807=ORIENTED_EDGE('',*,*,#38254,.T.);
#54808=ORIENTED_EDGE('',*,*,#38259,.F.);
#54809=ORIENTED_EDGE('',*,*,#38231,.T.);
#54810=ORIENTED_EDGE('',*,*,#38260,.T.);
#54811=ORIENTED_EDGE('',*,*,#38261,.F.);
#54812=ORIENTED_EDGE('',*,*,#38262,.F.);
#54813=ORIENTED_EDGE('',*,*,#38263,.T.);
#54814=ORIENTED_EDGE('',*,*,#38263,.F.);
#54815=ORIENTED_EDGE('',*,*,#38264,.F.);
#54816=ORIENTED_EDGE('',*,*,#38228,.F.);
#54817=ORIENTED_EDGE('',*,*,#38225,.F.);
#54818=ORIENTED_EDGE('',*,*,#38222,.F.);
#54819=ORIENTED_EDGE('',*,*,#38219,.F.);
#54820=ORIENTED_EDGE('',*,*,#38216,.F.);
#54821=ORIENTED_EDGE('',*,*,#38213,.F.);
#54822=ORIENTED_EDGE('',*,*,#38210,.F.);
#54823=ORIENTED_EDGE('',*,*,#38207,.F.);
#54824=ORIENTED_EDGE('',*,*,#38204,.F.);
#54825=ORIENTED_EDGE('',*,*,#38201,.F.);
#54826=ORIENTED_EDGE('',*,*,#38198,.F.);
#54827=ORIENTED_EDGE('',*,*,#38265,.F.);
#54828=ORIENTED_EDGE('',*,*,#38266,.T.);
#54829=ORIENTED_EDGE('',*,*,#38259,.T.);
#54830=ORIENTED_EDGE('',*,*,#38256,.T.);
#54831=ORIENTED_EDGE('',*,*,#38253,.T.);
#54832=ORIENTED_EDGE('',*,*,#38250,.T.);
#54833=ORIENTED_EDGE('',*,*,#38247,.T.);
#54834=ORIENTED_EDGE('',*,*,#38244,.T.);
#54835=ORIENTED_EDGE('',*,*,#38241,.T.);
#54836=ORIENTED_EDGE('',*,*,#38238,.T.);
#54837=ORIENTED_EDGE('',*,*,#38235,.T.);
#54838=ORIENTED_EDGE('',*,*,#38232,.T.);
#54839=ORIENTED_EDGE('',*,*,#38267,.T.);
#54840=ORIENTED_EDGE('',*,*,#38268,.T.);
#54841=ORIENTED_EDGE('',*,*,#38269,.T.);
#54842=ORIENTED_EDGE('',*,*,#38270,.T.);
#54843=ORIENTED_EDGE('',*,*,#38265,.T.);
#54844=ORIENTED_EDGE('',*,*,#38257,.T.);
#54845=ORIENTED_EDGE('',*,*,#38266,.F.);
#54846=ORIENTED_EDGE('',*,*,#38270,.F.);
#54847=ORIENTED_EDGE('',*,*,#38271,.T.);
#54848=ORIENTED_EDGE('',*,*,#38260,.F.);
#54849=ORIENTED_EDGE('',*,*,#38230,.F.);
#54850=ORIENTED_EDGE('',*,*,#38234,.F.);
#54851=ORIENTED_EDGE('',*,*,#38237,.F.);
#54852=ORIENTED_EDGE('',*,*,#38240,.F.);
#54853=ORIENTED_EDGE('',*,*,#38243,.F.);
#54854=ORIENTED_EDGE('',*,*,#38246,.F.);
#54855=ORIENTED_EDGE('',*,*,#38249,.F.);
#54856=ORIENTED_EDGE('',*,*,#38252,.F.);
#54857=ORIENTED_EDGE('',*,*,#38255,.F.);
#54858=ORIENTED_EDGE('',*,*,#38258,.F.);
#54859=ORIENTED_EDGE('',*,*,#38271,.F.);
#54860=ORIENTED_EDGE('',*,*,#38269,.F.);
#54861=ORIENTED_EDGE('',*,*,#38196,.F.);
#54862=ORIENTED_EDGE('',*,*,#38200,.F.);
#54863=ORIENTED_EDGE('',*,*,#38203,.F.);
#54864=ORIENTED_EDGE('',*,*,#38206,.F.);
#54865=ORIENTED_EDGE('',*,*,#38209,.F.);
#54866=ORIENTED_EDGE('',*,*,#38212,.F.);
#54867=ORIENTED_EDGE('',*,*,#38215,.F.);
#54868=ORIENTED_EDGE('',*,*,#38218,.F.);
#54869=ORIENTED_EDGE('',*,*,#38221,.F.);
#54870=ORIENTED_EDGE('',*,*,#38224,.F.);
#54871=ORIENTED_EDGE('',*,*,#38227,.F.);
#54872=ORIENTED_EDGE('',*,*,#38272,.F.);
#54873=ORIENTED_EDGE('',*,*,#38273,.F.);
#54874=ORIENTED_EDGE('',*,*,#38274,.T.);
#54875=ORIENTED_EDGE('',*,*,#38275,.F.);
#54876=ORIENTED_EDGE('',*,*,#38276,.T.);
#54877=ORIENTED_EDGE('',*,*,#38277,.F.);
#54878=ORIENTED_EDGE('',*,*,#38278,.F.);
#54879=ORIENTED_EDGE('',*,*,#38279,.T.);
#54880=ORIENTED_EDGE('',*,*,#38280,.F.);
#54881=ORIENTED_EDGE('',*,*,#38281,.F.);
#54882=ORIENTED_EDGE('',*,*,#38282,.T.);
#54883=ORIENTED_EDGE('',*,*,#38283,.F.);
#54884=ORIENTED_EDGE('',*,*,#38284,.F.);
#54885=ORIENTED_EDGE('',*,*,#38285,.T.);
#54886=ORIENTED_EDGE('',*,*,#38286,.F.);
#54887=ORIENTED_EDGE('',*,*,#38287,.F.);
#54888=ORIENTED_EDGE('',*,*,#38288,.T.);
#54889=ORIENTED_EDGE('',*,*,#38289,.F.);
#54890=ORIENTED_EDGE('',*,*,#38290,.F.);
#54891=ORIENTED_EDGE('',*,*,#38291,.T.);
#54892=ORIENTED_EDGE('',*,*,#38292,.F.);
#54893=ORIENTED_EDGE('',*,*,#38274,.F.);
#54894=ORIENTED_EDGE('',*,*,#38293,.F.);
#54895=ORIENTED_EDGE('',*,*,#38282,.F.);
#54896=ORIENTED_EDGE('',*,*,#38294,.F.);
#54897=ORIENTED_EDGE('',*,*,#38295,.F.);
#54898=ORIENTED_EDGE('',*,*,#38296,.F.);
#54899=ORIENTED_EDGE('',*,*,#38285,.F.);
#54900=ORIENTED_EDGE('',*,*,#38297,.F.);
#54901=ORIENTED_EDGE('',*,*,#38298,.F.);
#54902=ORIENTED_EDGE('',*,*,#38299,.F.);
#54903=ORIENTED_EDGE('',*,*,#38300,.F.);
#54904=ORIENTED_EDGE('',*,*,#38301,.F.);
#54905=ORIENTED_EDGE('',*,*,#38279,.F.);
#54906=ORIENTED_EDGE('',*,*,#38302,.F.);
#54907=ORIENTED_EDGE('',*,*,#38288,.F.);
#54908=ORIENTED_EDGE('',*,*,#38303,.F.);
#54909=ORIENTED_EDGE('',*,*,#38304,.F.);
#54910=ORIENTED_EDGE('',*,*,#38305,.F.);
#54911=ORIENTED_EDGE('',*,*,#38306,.F.);
#54912=ORIENTED_EDGE('',*,*,#38307,.F.);
#54913=ORIENTED_EDGE('',*,*,#38276,.F.);
#54914=ORIENTED_EDGE('',*,*,#38308,.F.);
#54915=ORIENTED_EDGE('',*,*,#38309,.F.);
#54916=ORIENTED_EDGE('',*,*,#38310,.F.);
#54917=ORIENTED_EDGE('',*,*,#38291,.F.);
#54918=ORIENTED_EDGE('',*,*,#38289,.T.);
#54919=ORIENTED_EDGE('',*,*,#38302,.T.);
#54920=ORIENTED_EDGE('',*,*,#38311,.F.);
#54921=ORIENTED_EDGE('',*,*,#38303,.T.);
#54922=ORIENTED_EDGE('',*,*,#38287,.T.);
#54923=ORIENTED_EDGE('',*,*,#38312,.T.);
#54924=ORIENTED_EDGE('',*,*,#38313,.T.);
#54925=ORIENTED_EDGE('',*,*,#38314,.F.);
#54926=ORIENTED_EDGE('',*,*,#38286,.T.);
#54927=ORIENTED_EDGE('',*,*,#38296,.T.);
#54928=ORIENTED_EDGE('',*,*,#38315,.F.);
#54929=ORIENTED_EDGE('',*,*,#38297,.T.);
#54930=ORIENTED_EDGE('',*,*,#38284,.T.);
#54931=ORIENTED_EDGE('',*,*,#38316,.T.);
#54932=ORIENTED_EDGE('',*,*,#38317,.T.);
#54933=ORIENTED_EDGE('',*,*,#38312,.F.);
#54934=ORIENTED_EDGE('',*,*,#38283,.T.);
#54935=ORIENTED_EDGE('',*,*,#38293,.T.);
#54936=ORIENTED_EDGE('',*,*,#38318,.F.);
#54937=ORIENTED_EDGE('',*,*,#38294,.T.);
#54938=ORIENTED_EDGE('',*,*,#38281,.T.);
#54939=ORIENTED_EDGE('',*,*,#38319,.T.);
#54940=ORIENTED_EDGE('',*,*,#38320,.T.);
#54941=ORIENTED_EDGE('',*,*,#38316,.F.);
#54942=ORIENTED_EDGE('',*,*,#38295,.T.);
#54943=ORIENTED_EDGE('',*,*,#38318,.T.);
#54944=ORIENTED_EDGE('',*,*,#38298,.T.);
#54945=ORIENTED_EDGE('',*,*,#38315,.T.);
#54946=ORIENTED_EDGE('',*,*,#38300,.T.);
#54947=ORIENTED_EDGE('',*,*,#38321,.T.);
#54948=ORIENTED_EDGE('',*,*,#38304,.T.);
#54949=ORIENTED_EDGE('',*,*,#38311,.T.);
#54950=ORIENTED_EDGE('',*,*,#38306,.T.);
#54951=ORIENTED_EDGE('',*,*,#38322,.T.);
#54952=ORIENTED_EDGE('',*,*,#38309,.T.);
#54953=ORIENTED_EDGE('',*,*,#38323,.T.);
#54954=ORIENTED_EDGE('',*,*,#38324,.F.);
#54955=ORIENTED_EDGE('',*,*,#38325,.T.);
#54956=ORIENTED_EDGE('',*,*,#38320,.F.);
#54957=ORIENTED_EDGE('',*,*,#38326,.T.);
#54958=ORIENTED_EDGE('',*,*,#38317,.F.);
#54959=ORIENTED_EDGE('',*,*,#38327,.T.);
#54960=ORIENTED_EDGE('',*,*,#38313,.F.);
#54961=ORIENTED_EDGE('',*,*,#38328,.T.);
#54962=ORIENTED_EDGE('',*,*,#38329,.F.);
#54963=ORIENTED_EDGE('',*,*,#38330,.T.);
#54964=ORIENTED_EDGE('',*,*,#38331,.F.);
#54965=ORIENTED_EDGE('',*,*,#38332,.T.);
#54966=ORIENTED_EDGE('',*,*,#38327,.F.);
#54967=ORIENTED_EDGE('',*,*,#38326,.F.);
#54968=ORIENTED_EDGE('',*,*,#38325,.F.);
#54969=ORIENTED_EDGE('',*,*,#38332,.F.);
#54970=ORIENTED_EDGE('',*,*,#38333,.T.);
#54971=ORIENTED_EDGE('',*,*,#38333,.F.);
#54972=ORIENTED_EDGE('',*,*,#38330,.F.);
#54973=ORIENTED_EDGE('',*,*,#38328,.F.);
#54974=ORIENTED_EDGE('',*,*,#38278,.T.);
#54975=ORIENTED_EDGE('',*,*,#38334,.T.);
#54976=ORIENTED_EDGE('',*,*,#38324,.T.);
#54977=ORIENTED_EDGE('',*,*,#38319,.F.);
#54978=ORIENTED_EDGE('',*,*,#38280,.T.);
#54979=ORIENTED_EDGE('',*,*,#38301,.T.);
#54980=ORIENTED_EDGE('',*,*,#38321,.F.);
#54981=ORIENTED_EDGE('',*,*,#38299,.T.);
#54982=ORIENTED_EDGE('',*,*,#38275,.T.);
#54983=ORIENTED_EDGE('',*,*,#38335,.T.);
#54984=ORIENTED_EDGE('',*,*,#38331,.T.);
#54985=ORIENTED_EDGE('',*,*,#38334,.F.);
#54986=ORIENTED_EDGE('',*,*,#38277,.T.);
#54987=ORIENTED_EDGE('',*,*,#38307,.T.);
#54988=ORIENTED_EDGE('',*,*,#38322,.F.);
#54989=ORIENTED_EDGE('',*,*,#38305,.T.);
#54990=ORIENTED_EDGE('',*,*,#38290,.T.);
#54991=ORIENTED_EDGE('',*,*,#38314,.T.);
#54992=ORIENTED_EDGE('',*,*,#38329,.T.);
#54993=ORIENTED_EDGE('',*,*,#38335,.F.);
#54994=ORIENTED_EDGE('',*,*,#38292,.T.);
#54995=ORIENTED_EDGE('',*,*,#38310,.T.);
#54996=ORIENTED_EDGE('',*,*,#38323,.F.);
#54997=ORIENTED_EDGE('',*,*,#38308,.T.);
#54998=ORIENTED_EDGE('',*,*,#38336,.F.);
#54999=ORIENTED_EDGE('',*,*,#38273,.T.);
#55000=ORIENTED_EDGE('',*,*,#38267,.F.);
#55001=ORIENTED_EDGE('',*,*,#38197,.F.);
#55002=ORIENTED_EDGE('',*,*,#38268,.F.);
#55003=ORIENTED_EDGE('',*,*,#38337,.T.);
#55004=ORIENTED_EDGE('',*,*,#38336,.T.);
#55005=ORIENTED_EDGE('',*,*,#38337,.F.);
#55006=ORIENTED_EDGE('',*,*,#38226,.T.);
#55007=ORIENTED_EDGE('',*,*,#38264,.T.);
#55008=ORIENTED_EDGE('',*,*,#38338,.F.);
#55009=ORIENTED_EDGE('',*,*,#38272,.T.);
#55010=ORIENTED_EDGE('',*,*,#38339,.F.);
#55011=ORIENTED_EDGE('',*,*,#38340,.T.);
#55012=ORIENTED_EDGE('',*,*,#38261,.T.);
#55013=ORIENTED_EDGE('',*,*,#38338,.T.);
#55014=ORIENTED_EDGE('',*,*,#38262,.T.);
#55015=ORIENTED_EDGE('',*,*,#38340,.F.);
#55016=ORIENTED_EDGE('',*,*,#38339,.T.);
#57117=B_SPLINE_SURFACE_WITH_KNOTS('',3,3,((#107449,#107450,#107451,#107452,
#107453,#107454,#107455,#107456,#107457,#107458,#107459,#107460,#107461,
#107462,#107463,#107464,#107465,#107466,#107467,#107468,#107469,#107470,
#107471,#107472,#107473,#107474,#107475,#107476,#107477,#107478,#107479,
#107480,#107481,#107482,#107483,#107484,#107485,#107486,#107487,#107488,
#107489,#107490,#107491,#107492,#107493,#107494,#107495,#107496,#107497,
#107498,#107499,#107500,#107501,#107502,#107503,#107504,#107505,#107506,
#107507,#107508,#107509,#107510,#107511,#107512,#107513,#107514,#107515,
#107516,#107517,#107518,#107519,#107520),(#107521,#107522,#107523,#107524,
#107525,#107526,#107527,#107528,#107529,#107530,#107531,#107532,#107533,
#107534,#107535,#107536,#107537,#107538,#107539,#107540,#107541,#107542,
#107543,#107544,#107545,#107546,#107547,#107548,#107549,#107550,#107551,
#107552,#107553,#107554,#107555,#107556,#107557,#107558,#107559,#107560,
#107561,#107562,#107563,#107564,#107565,#107566,#107567,#107568,#107569,
#107570,#107571,#107572,#107573,#107574,#107575,#107576,#107577,#107578,
#107579,#107580,#107581,#107582,#107583,#107584,#107585,#107586,#107587,
#107588,#107589,#107590,#107591,#107592),(#107593,#107594,#107595,#107596,
#107597,#107598,#107599,#107600,#107601,#107602,#107603,#107604,#107605,
#107606,#107607,#107608,#107609,#107610,#107611,#107612,#107613,#107614,
#107615,#107616,#107617,#107618,#107619,#107620,#107621,#107622,#107623,
#107624,#107625,#107626,#107627,#107628,#107629,#107630,#107631,#107632,
#107633,#107634,#107635,#107636,#107637,#107638,#107639,#107640,#107641,
#107642,#107643,#107644,#107645,#107646,#107647,#107648,#107649,#107650,
#107651,#107652,#107653,#107654,#107655,#107656,#107657,#107658,#107659,
#107660,#107661,#107662,#107663,#107664),(#107665,#107666,#107667,#107668,
#107669,#107670,#107671,#107672,#107673,#107674,#107675,#107676,#107677,
#107678,#107679,#107680,#107681,#107682,#107683,#107684,#107685,#107686,
#107687,#107688,#107689,#107690,#107691,#107692,#107693,#107694,#107695,
#107696,#107697,#107698,#107699,#107700,#107701,#107702,#107703,#107704,
#107705,#107706,#107707,#107708,#107709,#107710,#107711,#107712,#107713,
#107714,#107715,#107716,#107717,#107718,#107719,#107720,#107721,#107722,
#107723,#107724,#107725,#107726,#107727,#107728,#107729,#107730,#107731,
#107732,#107733,#107734,#107735,#107736)),.UNSPECIFIED.,.F.,.F.,.F.,(4,
4),(4,1,1,1,1,1,1,1,1,1,1,1,1,1,1,1,1,1,1,1,1,1,1,1,1,1,1,1,1,1,1,1,1,1,
1,1,1,1,1,1,1,1,1,1,1,1,1,1,1,1,1,1,1,1,1,1,1,1,1,1,1,1,1,1,1,1,1,1,1,4),
(0.,0.0329955678841871),(8.30203615430834,9.29240781985667,10.282779485405,
11.2731511509533,12.2635228165017,13.25389448205,14.2442661475984,15.2346378131467,
16.225009478695,17.2153811442434,18.2057528097917,19.19612447534,20.1864961408884,
21.1768678064367,22.1672394719851,23.1576111375334,24.1479828030817,25.1383544686301,
26.1287261341784,27.1190977997268,28.1094694652751,29.0998411308234,30.0902127963718,
31.0805844619201,32.0709561274684,33.0613277930168,34.0516994585651,35.0420711241134,
36.0324427896618,37.0228144552101,38.0131861207585,39.0035577863068,39.9939294518551,
40.9843011174035,41.9746727829518,42.9650444485002,43.9554161140485,44.9457877795968,
45.9361594451452,46.9265311106935,47.9169027762418,48.9072744417902,49.8976461073385,
50.8880177728869,51.8783894384352,52.8687611039835,53.8591327695319,54.8495044350802,
55.8398761006285,56.8302477661769,57.8206194317252,58.8109910972736,59.8013627628219,
60.7917344283702,61.7821060939186,62.7724777594669,63.7628494250152,64.7532210905636,
65.7435927561119,66.7339644216603,67.7243360872086,68.7147077527569,69.7050794183053,
70.6954510838536,71.685822749402,72.6761944149503,73.6665660804986,74.656937746047,
75.6473094115953,76.6376810771436),.UNSPECIFIED.);
#57118=B_SPLINE_SURFACE_WITH_KNOTS('',3,3,((#107939,#107940,#107941,#107942,
#107943,#107944,#107945,#107946,#107947,#107948,#107949,#107950,#107951,
#107952,#107953,#107954,#107955,#107956,#107957,#107958,#107959,#107960,
#107961,#107962,#107963,#107964,#107965,#107966,#107967,#107968,#107969,
#107970,#107971,#107972,#107973,#107974,#107975,#107976,#107977,#107978,
#107979,#107980,#107981,#107982,#107983,#107984,#107985,#107986,#107987,
#107988,#107989,#107990,#107991,#107992,#107993,#107994,#107995,#107996,
#107997,#107998,#107999,#108000,#108001,#108002,#108003,#108004,#108005,
#108006,#108007,#108008,#108009,#108010),(#108011,#108012,#108013,#108014,
#108015,#108016,#108017,#108018,#108019,#108020,#108021,#108022,#108023,
#108024,#108025,#108026,#108027,#108028,#108029,#108030,#108031,#108032,
#108033,#108034,#108035,#108036,#108037,#108038,#108039,#108040,#108041,
#108042,#108043,#108044,#108045,#108046,#108047,#108048,#108049,#108050,
#108051,#108052,#108053,#108054,#108055,#108056,#108057,#108058,#108059,
#108060,#108061,#108062,#108063,#108064,#108065,#108066,#108067,#108068,
#108069,#108070,#108071,#108072,#108073,#108074,#108075,#108076,#108077,
#108078,#108079,#108080,#108081,#108082),(#108083,#108084,#108085,#108086,
#108087,#108088,#108089,#108090,#108091,#108092,#108093,#108094,#108095,
#108096,#108097,#108098,#108099,#108100,#108101,#108102,#108103,#108104,
#108105,#108106,#108107,#108108,#108109,#108110,#108111,#108112,#108113,
#108114,#108115,#108116,#108117,#108118,#108119,#108120,#108121,#108122,
#108123,#108124,#108125,#108126,#108127,#108128,#108129,#108130,#108131,
#108132,#108133,#108134,#108135,#108136,#108137,#108138,#108139,#108140,
#108141,#108142,#108143,#108144,#108145,#108146,#108147,#108148,#108149,
#108150,#108151,#108152,#108153,#108154),(#108155,#108156,#108157,#108158,
#108159,#108160,#108161,#108162,#108163,#108164,#108165,#108166,#108167,
#108168,#108169,#108170,#108171,#108172,#108173,#108174,#108175,#108176,
#108177,#108178,#108179,#108180,#108181,#108182,#108183,#108184,#108185,
#108186,#108187,#108188,#108189,#108190,#108191,#108192,#108193,#108194,
#108195,#108196,#108197,#108198,#108199,#108200,#108201,#108202,#108203,
#108204,#108205,#108206,#108207,#108208,#108209,#108210,#108211,#108212,
#108213,#108214,#108215,#108216,#108217,#108218,#108219,#108220,#108221,
#108222,#108223,#108224,#108225,#108226)),.UNSPECIFIED.,.F.,.F.,.F.,(4,
4),(4,1,1,1,1,1,1,1,1,1,1,1,1,1,1,1,1,1,1,1,1,1,1,1,1,1,1,1,1,1,1,1,1,1,
1,1,1,1,1,1,1,1,1,1,1,1,1,1,1,1,1,1,1,1,1,1,1,1,1,1,1,1,1,1,1,1,1,1,1,4),
(0.,0.0329955678841871),(11.6159397475004,12.6063114130487,13.596683078597,
14.5870547441454,15.5774264096937,16.5677980752421,17.5581697407904,18.5485414063387,
19.5389130718871,20.5292847374354,21.5196564029837,22.5100280685321,23.5003997340804,
24.4907713996288,25.4811430651771,26.4715147307254,27.4618863962738,28.4522580618221,
29.4426297273704,30.4330013929188,31.4233730584671,32.4137447240155,33.4041163895638,
34.3944880551121,35.3848597206605,36.3752313862088,37.3656030517571,38.3559747173055,
39.3463463828538,40.3367180484022,41.3270897139505,42.3174613794988,43.3078330450472,
44.2982047105955,45.2885763761439,46.2789480416922,47.2693197072405,48.2596913727889,
49.2500630383372,50.2404347038855,51.2308063694339,52.2211780349822,53.2115497005306,
54.2019213660789,55.1922930316272,56.1826646971756,57.1730363627239,58.1634080282722,
59.1537796938206,60.1441513593689,61.1345230249173,62.1248946904656,63.1152663560139,
64.1056380215623,65.0960096871106,66.0863813526589,67.0767530182073,68.0671246837556,
69.057496349304,70.0478680148523,71.0382396804006,72.028611345949,73.0189830114973,
74.0093546770456,74.999726342594,75.9900980081423,76.9804696736907,77.970841339239,
78.9612130047873,79.9515846703357),.UNSPECIFIED.);
#60077=ADVANCED_FACE('',(#6977),#774,.T.);
#60078=ADVANCED_FACE('',(#6978),#775,.T.);
#60079=ADVANCED_FACE('',(#6979),#776,.T.);
#60080=ADVANCED_FACE('',(#6980),#777,.T.);
#60081=ADVANCED_FACE('',(#6981),#778,.T.);
#60082=ADVANCED_FACE('',(#6982),#779,.T.);
#60083=ADVANCED_FACE('',(#6983),#780,.T.);
#60084=ADVANCED_FACE('',(#6984),#781,.T.);
#60085=ADVANCED_FACE('',(#6985),#782,.T.);
#60086=ADVANCED_FACE('',(#6986),#783,.T.);
#60087=ADVANCED_FACE('',(#6987),#784,.T.);
#60088=ADVANCED_FACE('',(#6988),#785,.T.);
#60089=ADVANCED_FACE('',(#6989),#786,.T.);
#60090=ADVANCED_FACE('',(#6990),#787,.T.);
#60091=ADVANCED_FACE('',(#6991),#788,.T.);
#60092=ADVANCED_FACE('',(#6992),#789,.T.);
#60093=ADVANCED_FACE('',(#6993),#790,.T.);
#60094=ADVANCED_FACE('',(#6994),#791,.T.);
#60095=ADVANCED_FACE('',(#6995),#792,.T.);
#60096=ADVANCED_FACE('',(#6996),#793,.T.);
#60097=ADVANCED_FACE('',(#6997),#794,.T.);
#60098=ADVANCED_FACE('',(#6998),#3837,.F.);
#60099=ADVANCED_FACE('',(#6999),#57117,.F.);
#60100=ADVANCED_FACE('',(#7000),#3838,.T.);
#60101=ADVANCED_FACE('',(#7001),#795,.T.);
#60102=ADVANCED_FACE('',(#7002),#57118,.F.);
#60103=ADVANCED_FACE('',(#7003),#941,.F.);
#60104=ADVANCED_FACE('',(#7004),#796,.T.);
#60105=ADVANCED_FACE('',(#7005),#797,.T.);
#60106=ADVANCED_FACE('',(#7006),#798,.T.);
#60107=ADVANCED_FACE('',(#7007),#799,.T.);
#60108=ADVANCED_FACE('',(#7008),#800,.T.);
#60109=ADVANCED_FACE('',(#7009),#801,.T.);
#60110=ADVANCED_FACE('',(#7010),#3839,.F.);
#60111=ADVANCED_FACE('',(#7011),#3840,.F.);
#60112=ADVANCED_FACE('',(#7012),#3841,.F.);
#60113=ADVANCED_FACE('',(#7013),#3842,.T.);
#60114=ADVANCED_FACE('',(#7014),#3843,.T.);
#60115=ADVANCED_FACE('',(#7015),#3844,.T.);
#60116=ADVANCED_FACE('',(#7016),#3845,.T.);
#60117=ADVANCED_FACE('',(#7017),#3846,.T.);
#60118=ADVANCED_FACE('',(#7018),#3847,.T.);
#60119=ADVANCED_FACE('',(#7019),#3848,.F.);
#60120=ADVANCED_FACE('',(#7020),#3849,.F.);
#60121=ADVANCED_FACE('',(#7021),#3850,.F.);
#60122=ADVANCED_FACE('',(#7022),#3851,.F.);
#60123=ADVANCED_FACE('',(#7023),#3852,.F.);
#60124=ADVANCED_FACE('',(#7024),#3853,.F.);
#60125=ADVANCED_FACE('',(#7025),#942,.F.);
#60126=ADVANCED_FACE('',(#7026),#3854,.F.);
#60127=ADVANCED_FACE('',(#7027),#3855,.F.);
#60128=ADVANCED_FACE('',(#7028),#3856,.F.);
#60129=ADVANCED_FACE('',(#7029,#1854),#3857,.T.);
#60130=ADVANCED_FACE('',(#7030),#943,.T.);
#60131=ADVANCED_FACE('',(#7031),#802,.T.);
#60132=ADVANCED_FACE('',(#7032),#944,.T.);
#60133=ADVANCED_FACE('',(#7033),#3858,.T.);
#60405=CLOSED_SHELL('',(#60077,#60078,#60079,#60080,#60081,#60082,#60083,
#60084,#60085,#60086,#60087,#60088,#60089,#60090,#60091,#60092,#60093,#60094,
#60095,#60096,#60097,#60098,#60099,#60100,#60101,#60102,#60103,#60104,#60105,
#60106,#60107,#60108,#60109,#60110,#60111,#60112,#60113,#60114,#60115,#60116,
#60117,#60118,#60119,#60120,#60121,#60122,#60123,#60124,#60125,#60126,#60127,
#60128,#60129,#60130,#60131,#60132,#60133));
#63259=AXIS2_PLACEMENT_3D('',#106507,#74731,#74732);
#63260=AXIS2_PLACEMENT_3D('',#106508,#74733,#74734);
#63261=AXIS2_PLACEMENT_3D('',#106524,#74736,#74737);
#63262=AXIS2_PLACEMENT_3D('',#106532,#74738,#74739);
#63263=AXIS2_PLACEMENT_3D('',#106580,#74741,#74742);
#63264=AXIS2_PLACEMENT_3D('',#106628,#74744,#74745);
#63265=AXIS2_PLACEMENT_3D('',#106682,#74747,#74748);
#63266=AXIS2_PLACEMENT_3D('',#106730,#74750,#74751);
#63267=AXIS2_PLACEMENT_3D('',#106778,#74753,#74754);
#63268=AXIS2_PLACEMENT_3D('',#106832,#74756,#74757);
#63269=AXIS2_PLACEMENT_3D('',#106880,#74759,#74760);
#63270=AXIS2_PLACEMENT_3D('',#106928,#74762,#74763);
#63271=AXIS2_PLACEMENT_3D('',#106982,#74765,#74766);
#63272=AXIS2_PLACEMENT_3D('',#107030,#74768,#74769);
#63273=AXIS2_PLACEMENT_3D('',#107045,#74771,#74772);
#63274=AXIS2_PLACEMENT_3D('',#107054,#74773,#74774);
#63275=AXIS2_PLACEMENT_3D('',#107079,#74776,#74777);
#63276=AXIS2_PLACEMENT_3D('',#107104,#74779,#74780);
#63277=AXIS2_PLACEMENT_3D('',#107128,#74782,#74783);
#63278=AXIS2_PLACEMENT_3D('',#107153,#74785,#74786);
#63279=AXIS2_PLACEMENT_3D('',#107178,#74788,#74789);
#63280=AXIS2_PLACEMENT_3D('',#107202,#74791,#74792);
#63281=AXIS2_PLACEMENT_3D('',#107227,#74794,#74795);
#63282=AXIS2_PLACEMENT_3D('',#107252,#74797,#74798);
#63283=AXIS2_PLACEMENT_3D('',#107276,#74800,#74801);
#63284=AXIS2_PLACEMENT_3D('',#107364,#74802,#74803);
#63285=AXIS2_PLACEMENT_3D('',#107366,#74804,#74805);
#63286=AXIS2_PLACEMENT_3D('',#107842,#74806,#74807);
#63287=AXIS2_PLACEMENT_3D('',#107844,#74808,#74809);
#63288=AXIS2_PLACEMENT_3D('',#107845,#74810,#74811);
#63289=AXIS2_PLACEMENT_3D('',#107929,#74812,#74813);
#63290=AXIS2_PLACEMENT_3D('',#107930,#74814,#74815);
#63291=AXIS2_PLACEMENT_3D('',#108234,#74816,#74817);
#63292=AXIS2_PLACEMENT_3D('',#108236,#74818,#74819);
#63293=AXIS2_PLACEMENT_3D('',#108244,#74821,#74822);
#63294=AXIS2_PLACEMENT_3D('',#108254,#74823,#74824);
#63295=AXIS2_PLACEMENT_3D('',#108264,#74825,#74826);
#63296=AXIS2_PLACEMENT_3D('',#108274,#74827,#74828);
#63297=AXIS2_PLACEMENT_3D('',#108284,#74829,#74830);
#63298=AXIS2_PLACEMENT_3D('',#108294,#74831,#74832);
#63299=AXIS2_PLACEMENT_3D('',#108298,#74833,#74834);
#63300=AXIS2_PLACEMENT_3D('',#108303,#74837,#74838);
#63301=AXIS2_PLACEMENT_3D('',#108304,#74839,#74840);
#63302=AXIS2_PLACEMENT_3D('',#108309,#74843,#74844);
#63303=AXIS2_PLACEMENT_3D('',#108310,#74845,#74846);
#63304=AXIS2_PLACEMENT_3D('',#108314,#74848,#74849);
#63305=AXIS2_PLACEMENT_3D('',#108316,#74851,#74852);
#63306=AXIS2_PLACEMENT_3D('',#108321,#74855,#74856);
#63307=AXIS2_PLACEMENT_3D('',#108322,#74857,#74858);
#63308=AXIS2_PLACEMENT_3D('',#108326,#74860,#74861);
#63309=AXIS2_PLACEMENT_3D('',#108328,#74863,#74864);
#63310=AXIS2_PLACEMENT_3D('',#108332,#74866,#74867);
#63311=AXIS2_PLACEMENT_3D('',#108334,#74869,#74870);
#63312=AXIS2_PLACEMENT_3D('',#108341,#74875,#74876);
#63313=AXIS2_PLACEMENT_3D('',#108346,#74880,#74881);
#63314=AXIS2_PLACEMENT_3D('',#108351,#74885,#74886);
#63315=AXIS2_PLACEMENT_3D('',#108352,#74887,#74888);
#63316=AXIS2_PLACEMENT_3D('',#108353,#74889,#74890);
#63317=AXIS2_PLACEMENT_3D('',#108355,#74892,#74893);
#63318=AXIS2_PLACEMENT_3D('',#108356,#74894,#74895);
#63319=AXIS2_PLACEMENT_3D('',#108358,#74897,#74898);
#63320=AXIS2_PLACEMENT_3D('',#108360,#74900,#74901);
#63321=AXIS2_PLACEMENT_3D('',#108363,#74903,#74904);
#63322=AXIS2_PLACEMENT_3D('',#108364,#74905,#74906);
#63323=AXIS2_PLACEMENT_3D('',#108365,#74907,#74908);
#63324=AXIS2_PLACEMENT_3D('',#108366,#74909,#74910);
#63325=AXIS2_PLACEMENT_3D('',#108367,#74911,#74912);
#63326=AXIS2_PLACEMENT_3D('',#108368,#74913,#74914);
#63327=AXIS2_PLACEMENT_3D('',#108369,#74915,#74916);
#63328=AXIS2_PLACEMENT_3D('',#108370,#74917,#74918);
#63329=AXIS2_PLACEMENT_3D('',#108373,#74920,#74921);
#63330=AXIS2_PLACEMENT_3D('',#108374,#74922,#74923);
#63331=AXIS2_PLACEMENT_3D('',#108376,#74925,#74926);
#63332=AXIS2_PLACEMENT_3D('',#108377,#74927,#74928);
#63333=AXIS2_PLACEMENT_3D('',#108380,#74930,#74931);
#63334=AXIS2_PLACEMENT_3D('',#108382,#74933,#74934);
#63335=AXIS2_PLACEMENT_3D('',#108384,#74936,#74937);
#63336=AXIS2_PLACEMENT_3D('',#108385,#74938,#74939);
#63337=AXIS2_PLACEMENT_3D('',#108387,#74940,#74941);
#63338=AXIS2_PLACEMENT_3D('',#108388,#74942,#74943);
#63339=AXIS2_PLACEMENT_3D('',#108390,#74945,#74946);
#63340=AXIS2_PLACEMENT_3D('',#108391,#74947,#74948);
#63341=AXIS2_PLACEMENT_3D('',#108392,#74949,#74950);
#63342=AXIS2_PLACEMENT_3D('',#108394,#74951,#74952);
#63343=AXIS2_PLACEMENT_3D('',#108396,#74954,#74955);
#74731=DIRECTION('axis',(0.,0.,1.));
#74732=DIRECTION('refdir',(1.,0.,0.));
#74733=DIRECTION('center_axis',(0.,0.,1.));
#74734=DIRECTION('ref_axis',(1.,0.,0.));
#74735=DIRECTION('',(0.,0.,-1.));
#74736=DIRECTION('center_axis',(0.,0.,1.));
#74737=DIRECTION('ref_axis',(1.,0.,0.));
#74738=DIRECTION('center_axis',(0.,0.,1.));
#74739=DIRECTION('ref_axis',(1.,0.,0.));
#74740=DIRECTION('',(0.,0.,-1.));
#74741=DIRECTION('center_axis',(0.,0.,1.));
#74742=DIRECTION('ref_axis',(1.,0.,0.));
#74743=DIRECTION('',(0.,0.,-1.));
#74744=DIRECTION('center_axis',(0.,0.,1.));
#74745=DIRECTION('ref_axis',(1.,0.,0.));
#74746=DIRECTION('',(0.,0.,-1.));
#74747=DIRECTION('center_axis',(0.,0.,1.));
#74748=DIRECTION('ref_axis',(1.,0.,0.));
#74749=DIRECTION('',(0.,0.,-1.));
#74750=DIRECTION('center_axis',(0.,0.,1.));
#74751=DIRECTION('ref_axis',(1.,0.,0.));
#74752=DIRECTION('',(0.,0.,-1.));
#74753=DIRECTION('center_axis',(0.,0.,1.));
#74754=DIRECTION('ref_axis',(1.,0.,0.));
#74755=DIRECTION('',(0.,0.,-1.));
#74756=DIRECTION('center_axis',(0.,0.,1.));
#74757=DIRECTION('ref_axis',(1.,0.,0.));
#74758=DIRECTION('',(0.,0.,-1.));
#74759=DIRECTION('center_axis',(0.,0.,1.));
#74760=DIRECTION('ref_axis',(1.,0.,0.));
#74761=DIRECTION('',(0.,0.,-1.));
#74762=DIRECTION('center_axis',(0.,0.,1.));
#74763=DIRECTION('ref_axis',(1.,0.,0.));
#74764=DIRECTION('',(0.,0.,-1.));
#74765=DIRECTION('center_axis',(0.,0.,1.));
#74766=DIRECTION('ref_axis',(1.,0.,0.));
#74767=DIRECTION('',(0.,0.,-1.));
#74768=DIRECTION('center_axis',(0.,0.,1.));
#74769=DIRECTION('ref_axis',(0.945752973643215,-0.324886615367603,0.));
#74770=DIRECTION('',(0.,0.,1.));
#74771=DIRECTION('center_axis',(0.,0.,1.));
#74772=DIRECTION('ref_axis',(1.,6.22158519424838E-14,0.));
#74773=DIRECTION('center_axis',(0.,0.,1.));
#74774=DIRECTION('ref_axis',(1.,6.22158519424838E-14,0.));
#74775=DIRECTION('',(0.,0.,1.));
#74776=DIRECTION('center_axis',(0.,0.,1.));
#74777=DIRECTION('ref_axis',(1.,6.22158519424838E-14,0.));
#74778=DIRECTION('',(0.,0.,1.));
#74779=DIRECTION('center_axis',(0.,0.,1.));
#74780=DIRECTION('ref_axis',(1.,6.22158519424838E-14,0.));
#74781=DIRECTION('',(0.,0.,1.));
#74782=DIRECTION('center_axis',(0.,0.,1.));
#74783=DIRECTION('ref_axis',(1.,6.22158519424838E-14,0.));
#74784=DIRECTION('',(0.,0.,1.));
#74785=DIRECTION('center_axis',(0.,0.,1.));
#74786=DIRECTION('ref_axis',(1.,6.22158519424838E-14,0.));
#74787=DIRECTION('',(0.,0.,1.));
#74788=DIRECTION('center_axis',(0.,0.,1.));
#74789=DIRECTION('ref_axis',(1.,6.22158519424838E-14,0.));
#74790=DIRECTION('',(0.,0.,1.));
#74791=DIRECTION('center_axis',(0.,0.,1.));
#74792=DIRECTION('ref_axis',(1.,6.22158519424838E-14,0.));
#74793=DIRECTION('',(0.,0.,1.));
#74794=DIRECTION('center_axis',(0.,0.,1.));
#74795=DIRECTION('ref_axis',(1.,6.22158519424838E-14,0.));
#74796=DIRECTION('',(0.,0.,1.));
#74797=DIRECTION('center_axis',(0.,0.,1.));
#74798=DIRECTION('ref_axis',(1.,6.22158519424838E-14,0.));
#74799=DIRECTION('',(0.,0.,1.));
#74800=DIRECTION('center_axis',(0.,0.,1.));
#74801=DIRECTION('ref_axis',(1.,0.,0.));
#74802=DIRECTION('center_axis',(0.,0.,-1.));
#74803=DIRECTION('ref_axis',(1.,0.,0.));
#74804=DIRECTION('center_axis',(0.,0.,-1.));
#74805=DIRECTION('ref_axis',(1.,0.,0.));
#74806=DIRECTION('center_axis',(0.,0.,1.));
#74807=DIRECTION('ref_axis',(1.,0.,0.));
#74808=DIRECTION('center_axis',(0.,0.,1.));
#74809=DIRECTION('ref_axis',(1.,0.,0.));
#74810=DIRECTION('center_axis',(0.,0.,1.));
#74811=DIRECTION('ref_axis',(1.,0.,0.));
#74812=DIRECTION('center_axis',(0.,0.,-1.));
#74813=DIRECTION('ref_axis',(1.,6.22158519424838E-14,0.));
#74814=DIRECTION('center_axis',(0.,0.,1.));
#74815=DIRECTION('ref_axis',(1.,6.22158519424838E-14,0.));
#74816=DIRECTION('center_axis',(0.,0.,-1.));
#74817=DIRECTION('ref_axis',(1.,0.,0.));
#74818=DIRECTION('center_axis',(0.,0.,1.));
#74819=DIRECTION('ref_axis',(1.,0.,0.));
#74820=DIRECTION('',(0.707106781186573,8.65956056235524E-17,0.707106781186522));
#74821=DIRECTION('center_axis',(0.,0.,1.));
#74822=DIRECTION('ref_axis',(1.,0.,0.));
#74823=DIRECTION('center_axis',(0.,0.,1.));
#74824=DIRECTION('ref_axis',(1.,0.,0.));
#74825=DIRECTION('center_axis',(0.,0.,1.));
#74826=DIRECTION('ref_axis',(1.,0.,0.));
#74827=DIRECTION('center_axis',(0.,0.,1.));
#74828=DIRECTION('ref_axis',(1.,0.,0.));
#74829=DIRECTION('center_axis',(0.,0.,1.));
#74830=DIRECTION('ref_axis',(1.,0.,0.));
#74831=DIRECTION('center_axis',(0.,0.,1.));
#74832=DIRECTION('ref_axis',(1.,0.,0.));
#74833=DIRECTION('center_axis',(0.,0.,1.));
#74834=DIRECTION('ref_axis',(1.,0.,0.));
#74835=DIRECTION('',(0.,0.,-1.));
#74836=DIRECTION('',(0.,0.,1.));
#74837=DIRECTION('center_axis',(0.,0.,-1.));
#74838=DIRECTION('ref_axis',(1.,0.,0.));
#74839=DIRECTION('center_axis',(0.,0.,1.));
#74840=DIRECTION('ref_axis',(1.,0.,0.));
#74841=DIRECTION('',(0.,0.,-1.));
#74842=DIRECTION('',(0.,0.,1.));
#74843=DIRECTION('center_axis',(0.,0.,-1.));
#74844=DIRECTION('ref_axis',(1.,0.,0.));
#74845=DIRECTION('center_axis',(0.,0.,1.));
#74846=DIRECTION('ref_axis',(1.,0.,0.));
#74847=DIRECTION('',(0.,0.,1.));
#74848=DIRECTION('center_axis',(0.,0.,-1.));
#74849=DIRECTION('ref_axis',(1.,0.,0.));
#74850=DIRECTION('',(0.,0.,-1.));
#74851=DIRECTION('center_axis',(0.,0.,1.));
#74852=DIRECTION('ref_axis',(1.,0.,0.));
#74853=DIRECTION('',(0.,0.,-1.));
#74854=DIRECTION('',(0.,0.,1.));
#74855=DIRECTION('center_axis',(0.,0.,-1.));
#74856=DIRECTION('ref_axis',(1.,0.,0.));
#74857=DIRECTION('center_axis',(0.,0.,1.));
#74858=DIRECTION('ref_axis',(1.,0.,0.));
#74859=DIRECTION('',(0.,0.,1.));
#74860=DIRECTION('center_axis',(0.,0.,-1.));
#74861=DIRECTION('ref_axis',(1.,0.,0.));
#74862=DIRECTION('',(0.,0.,-1.));
#74863=DIRECTION('center_axis',(0.,0.,1.));
#74864=DIRECTION('ref_axis',(1.,0.,0.));
#74865=DIRECTION('',(0.,0.,1.));
#74866=DIRECTION('center_axis',(0.,0.,-1.));
#74867=DIRECTION('ref_axis',(1.,0.,0.));
#74868=DIRECTION('',(0.,0.,-1.));
#74869=DIRECTION('center_axis',(0.,1.,0.));
#74870=DIRECTION('ref_axis',(-1.,0.,0.));
#74871=DIRECTION('',(-1.,0.,0.));
#74872=DIRECTION('',(0.,0.,1.));
#74873=DIRECTION('',(-1.,0.,0.));
#74874=DIRECTION('',(0.,0.,1.));
#74875=DIRECTION('center_axis',(0.86602540378444,0.499999999999998,0.));
#74876=DIRECTION('ref_axis',(-0.499999999999998,0.86602540378444,0.));
#74877=DIRECTION('',(-0.499999999999998,0.86602540378444,0.));
#74878=DIRECTION('',(0.,0.,1.));
#74879=DIRECTION('',(-0.499999999999998,0.86602540378444,0.));
#74880=DIRECTION('center_axis',(0.86602540378444,-0.499999999999998,0.));
#74881=DIRECTION('ref_axis',(0.499999999999998,0.86602540378444,0.));
#74882=DIRECTION('',(0.499999999999998,0.86602540378444,0.));
#74883=DIRECTION('',(0.,0.,1.));
#74884=DIRECTION('',(0.499999999999998,0.86602540378444,0.));
#74885=DIRECTION('center_axis',(0.,0.,-1.));
#74886=DIRECTION('ref_axis',(-1.,0.,0.));
#74887=DIRECTION('center_axis',(0.,0.,-1.));
#74888=DIRECTION('ref_axis',(-1.,0.,0.));
#74889=DIRECTION('center_axis',(0.,0.,-1.));
#74890=DIRECTION('ref_axis',(-1.,0.,0.));
#74891=DIRECTION('',(1.,0.,0.));
#74892=DIRECTION('center_axis',(0.,0.,-1.));
#74893=DIRECTION('ref_axis',(-1.,0.,0.));
#74894=DIRECTION('center_axis',(0.,0.,-1.));
#74895=DIRECTION('ref_axis',(-1.,0.,0.));
#74896=DIRECTION('',(0.499999999999983,-0.866025403784448,0.));
#74897=DIRECTION('center_axis',(0.,0.,-1.));
#74898=DIRECTION('ref_axis',(-1.,0.,0.));
#74899=DIRECTION('',(-0.499999999999983,-0.866025403784448,0.));
#74900=DIRECTION('center_axis',(0.,0.,-1.));
#74901=DIRECTION('ref_axis',(-1.,0.,0.));
#74902=DIRECTION('',(1.,0.,0.));
#74903=DIRECTION('center_axis',(0.,0.,1.));
#74904=DIRECTION('ref_axis',(1.,0.,0.));
#74905=DIRECTION('center_axis',(0.,0.,-1.));
#74906=DIRECTION('ref_axis',(-1.,0.,0.));
#74907=DIRECTION('center_axis',(0.,0.,1.));
#74908=DIRECTION('ref_axis',(1.,0.,0.));
#74909=DIRECTION('center_axis',(0.,0.,-1.));
#74910=DIRECTION('ref_axis',(-1.,0.,0.));
#74911=DIRECTION('center_axis',(0.,0.,1.));
#74912=DIRECTION('ref_axis',(1.,0.,0.));
#74913=DIRECTION('center_axis',(0.,0.,-1.));
#74914=DIRECTION('ref_axis',(-1.,0.,0.));
#74915=DIRECTION('center_axis',(0.,0.,1.));
#74916=DIRECTION('ref_axis',(1.,0.,0.));
#74917=DIRECTION('center_axis',(0.,0.,-1.));
#74918=DIRECTION('ref_axis',(-1.,0.,0.));
#74919=DIRECTION('',(-0.499999999999983,-0.866025403784448,0.));
#74920=DIRECTION('center_axis',(0.,0.,1.));
#74921=DIRECTION('ref_axis',(1.,0.,0.));
#74922=DIRECTION('center_axis',(0.,0.,-1.));
#74923=DIRECTION('ref_axis',(-1.,0.,0.));
#74924=DIRECTION('',(0.499999999999983,-0.866025403784448,0.));
#74925=DIRECTION('center_axis',(0.,0.,1.));
#74926=DIRECTION('ref_axis',(1.,0.,0.));
#74927=DIRECTION('center_axis',(0.,0.,-1.));
#74928=DIRECTION('ref_axis',(1.,0.,0.));
#74929=DIRECTION('',(0.85716730070211,1.04972719113862E-16,0.515038074910057));
#74930=DIRECTION('center_axis',(0.,-1.,0.));
#74931=DIRECTION('ref_axis',(1.,0.,0.));
#74932=DIRECTION('',(0.,0.,1.));
#74933=DIRECTION('center_axis',(-0.866025403784449,-0.499999999999983,0.));
#74934=DIRECTION('ref_axis',(0.499999999999983,-0.866025403784448,0.));
#74935=DIRECTION('',(0.,0.,1.));
#74936=DIRECTION('center_axis',(-0.866025403784449,0.499999999999983,0.));
#74937=DIRECTION('ref_axis',(-0.499999999999983,-0.866025403784448,0.));
#74938=DIRECTION('center_axis',(0.,0.,-1.));
#74939=DIRECTION('ref_axis',(-1.,0.,0.));
#74940=DIRECTION('center_axis',(0.,0.,1.));
#74941=DIRECTION('ref_axis',(1.,0.,0.));
#74942=DIRECTION('center_axis',(0.,0.,1.));
#74943=DIRECTION('ref_axis',(1.,0.,0.));
#74944=DIRECTION('',(0.70710678118654,8.65956056235484E-17,-0.707106781186555));
#74945=DIRECTION('center_axis',(0.,0.,1.));
#74946=DIRECTION('ref_axis',(1.,0.,0.));
#74947=DIRECTION('center_axis',(0.,0.,-1.));
#74948=DIRECTION('ref_axis',(1.,0.,0.));
#74949=DIRECTION('center_axis',(0.,0.,-1.));
#74950=DIRECTION('ref_axis',(1.,0.,0.));
#74951=DIRECTION('center_axis',(0.,0.,1.));
#74952=DIRECTION('ref_axis',(1.,0.,0.));
#74953=DIRECTION('',(-0.707106781186541,-8.65956056235486E-17,-0.707106781186554));
#74954=DIRECTION('center_axis',(0.,0.,1.));
#74955=DIRECTION('ref_axis',(1.,0.,0.));
#106507=CARTESIAN_POINT('',(0.,0.,0.));
#106508=CARTESIAN_POINT('Origin',(98.,10.75,11.7549960127668));
#106509=CARTESIAN_POINT('',(96.5351020985542,10.7510579807298,9.27915105860971));
#106510=CARTESIAN_POINT('',(96.5354401179964,10.7513381115446,9.20784096692389));
#106511=CARTESIAN_POINT('',(96.5365,10.75,11.7549960127668));
#106512=CARTESIAN_POINT('',(98.6347992875354,12.0698446533255,9.1184960127668));
#106513=CARTESIAN_POINT('Ctrl Pts',(96.5351020985542,10.7510579807298,9.27915105860971));
#106514=CARTESIAN_POINT('Ctrl Pts',(96.5346060590799,10.8145630912322,9.27568846090188));
#106515=CARTESIAN_POINT('Ctrl Pts',(96.5383821988364,10.878006616392,9.27222586319404));
#106516=CARTESIAN_POINT('Ctrl Pts',(96.5466319128065,10.9408598239014,9.26876326548621));
#106517=CARTESIAN_POINT('Ctrl Pts',(96.609221767305,11.4177215826278,9.24249284114118));
#106518=CARTESIAN_POINT('Ctrl Pts',(96.9293160773523,11.8606039284948,9.21622241679615));
#106519=CARTESIAN_POINT('Ctrl Pts',(97.3625071015607,12.069892529637,9.18995199245112));
#106520=CARTESIAN_POINT('Ctrl Pts',(97.7552693021089,12.2596486578589,9.16613333255634));
#106521=CARTESIAN_POINT('Ctrl Pts',(98.2410031353653,12.2573780592344,9.14231467266158));
#106522=CARTESIAN_POINT('Ctrl Pts',(98.6355914804955,12.0706490290142,9.1184960127668));
#106523=CARTESIAN_POINT('',(97.3659929054248,12.0690402776368,9.1184960127668));
#106524=CARTESIAN_POINT('Origin',(98.,10.75,9.1184960127668));
#106525=CARTESIAN_POINT('Ctrl Pts',(97.3659929054248,12.0690402776368,9.1184960127668));
#106526=CARTESIAN_POINT('Ctrl Pts',(96.930546199862,11.8597393902289,9.14476643711183));
#106527=CARTESIAN_POINT('Ctrl Pts',(96.6105106946804,11.419616133128,9.17103686145686));
#106528=CARTESIAN_POINT('Ctrl Pts',(96.5472508070897,10.9435820611701,9.19730728580189));
#106529=CARTESIAN_POINT('Ctrl Pts',(96.5387956780449,10.8799567582901,9.20081851284256));
#106530=CARTESIAN_POINT('Ctrl Pts',(96.5349276407975,10.8156899373181,9.20432973988323));
#106531=CARTESIAN_POINT('Ctrl Pts',(96.5354401179964,10.7513381115446,9.20784096692389));
#106532=CARTESIAN_POINT('Origin',(98.,10.75,11.7549960127668));
#106533=CARTESIAN_POINT('',(96.5387662976346,10.750184760568,9.7791510586097));
#106534=CARTESIAN_POINT('',(96.5387723473756,10.7501752126031,9.70784096692389));
#106535=CARTESIAN_POINT('',(96.5365,10.75,11.7549960127668));
#106536=CARTESIAN_POINT('Ctrl Pts',(96.5387662976346,10.750184760568,9.7791510586097));
#106537=CARTESIAN_POINT('Ctrl Pts',(96.538503535619,10.9810513320239,9.76664434030537));
#106538=CARTESIAN_POINT('Ctrl Pts',(96.590063734169,11.2118067540368,9.75413762200105));
#106539=CARTESIAN_POINT('Ctrl Pts',(96.6940778839653,11.415818168987,9.74163090369672));
#106540=CARTESIAN_POINT('Ctrl Pts',(96.9125601257928,11.8443451663622,9.71536047935169));
#106541=CARTESIAN_POINT('Ctrl Pts',(97.3624755610563,12.1548743616133,9.68909005500666));
#106542=CARTESIAN_POINT('Ctrl Pts',(97.8406352022483,12.20717006172,9.66281963066163));
#106543=CARTESIAN_POINT('Ctrl Pts',(98.3187948434403,12.2594657618267,9.63654920631661));
#106544=CARTESIAN_POINT('Ctrl Pts',(98.8251986905609,12.053527966789,9.61027878197158));
#106545=CARTESIAN_POINT('Ctrl Pts',(99.1311396738187,11.6823507781742,9.58400835762655));
#106546=CARTESIAN_POINT('Ctrl Pts',(99.4370806570765,11.3111735895595,9.55773793328152));
#106547=CARTESIAN_POINT('Ctrl Pts',(99.5425587764715,10.7747570073677,9.53146750893649));
#106548=CARTESIAN_POINT('Ctrl Pts',(99.3999470419584,10.3153816915692,9.50519708459146));
#106549=CARTESIAN_POINT('Ctrl Pts',(99.2573353074454,9.85600637577063,9.47892666024643));
#106550=CARTESIAN_POINT('Ctrl Pts',(98.8666337190244,9.47367232636532,9.4526562359014));
#106551=CARTESIAN_POINT('Ctrl Pts',(98.4042727797815,9.3410015425033,9.42638581155638));
#106552=CARTESIAN_POINT('Ctrl Pts',(97.9419118405387,9.20833075864129,9.40011538721135));
#106553=CARTESIAN_POINT('Ctrl Pts',(97.4078915504739,9.32532324032258,9.37384496286631));
#106554=CARTESIAN_POINT('Ctrl Pts',(97.0434241049163,9.63924006695603,9.34757453852129));
#106555=CARTESIAN_POINT('Ctrl Pts',(96.7269956299132,9.91178079436568,9.32476671188409));
#106556=CARTESIAN_POINT('Ctrl Pts',(96.5383694669553,10.3327554018202,9.3019588852469));
#106557=CARTESIAN_POINT('Ctrl Pts',(96.5351020985542,10.7510579807298,9.27915105860971));
#106558=CARTESIAN_POINT('Ctrl Pts',(96.5354401179964,10.7513381115446,9.20784096692389));
#106559=CARTESIAN_POINT('Ctrl Pts',(96.5387619110758,10.3342201403306,9.23060016422825));
#106560=CARTESIAN_POINT('Ctrl Pts',(96.726127496539,9.91353076072674,9.25335936153261));
#106561=CARTESIAN_POINT('Ctrl Pts',(97.0412798458648,9.64082474825794,9.27611855883697));
#106562=CARTESIAN_POINT('Ctrl Pts',(97.4050530422302,9.32604639411874,9.302388983182));
#106563=CARTESIAN_POINT('Ctrl Pts',(97.939083704961,9.20843457265531,9.32865940752703));
#106564=CARTESIAN_POINT('Ctrl Pts',(98.4017442787636,9.34034906364773,9.35492983187206));
#106565=CARTESIAN_POINT('Ctrl Pts',(98.8644048525662,9.47226355464014,9.38120025621709));
#106566=CARTESIAN_POINT('Ctrl Pts',(99.2556953374407,9.85370435808839,9.40747068056212));
#106567=CARTESIAN_POINT('Ctrl Pts',(99.3991207985907,10.3127728125,9.43374110490715));
#106568=CARTESIAN_POINT('Ctrl Pts',(99.5425462597407,10.7718412669117,9.46001152925217));
#106569=CARTESIAN_POINT('Ctrl Pts',(99.4381066971662,11.3085373722868,9.4862819535972));
#106570=CARTESIAN_POINT('Ctrl Pts',(99.1328605939268,11.6802968798121,9.51255237794223));
#106571=CARTESIAN_POINT('Ctrl Pts',(98.8276144906875,12.0520563873375,9.53882280228726));
#106572=CARTESIAN_POINT('Ctrl Pts',(98.3215618467832,12.2588792970132,9.56509322663229));
#106573=CARTESIAN_POINT('Ctrl Pts',(97.8433002185608,12.2074494086105,9.59136365097732));
#106574=CARTESIAN_POINT('Ctrl Pts',(97.3650385903383,12.1560195202078,9.61763407532235));
#106575=CARTESIAN_POINT('Ctrl Pts',(96.9145679777977,11.8463368337266,9.64390449966737));
#106576=CARTESIAN_POINT('Ctrl Pts',(96.6953038636642,11.4182164216731,9.6701749240124));
#106577=CARTESIAN_POINT('Ctrl Pts',(96.5905116021786,11.2136060760883,9.68273027164956));
#106578=CARTESIAN_POINT('Ctrl Pts',(96.5385302134461,10.9819428591635,9.69528561928673));
#106579=CARTESIAN_POINT('Ctrl Pts',(96.5387723473756,10.7501752126031,9.70784096692389));
#106580=CARTESIAN_POINT('Origin',(98.,10.75,11.7549960127668));
#106581=CARTESIAN_POINT('',(96.5357076024386,10.7488070530836,10.2791510586097));
#106582=CARTESIAN_POINT('',(96.5356817146954,10.7488128621349,10.2078409669239));
#106583=CARTESIAN_POINT('',(96.5365,10.75,11.7549960127668));
#106584=CARTESIAN_POINT('Ctrl Pts',(96.5357076024386,10.7488070530836,10.2791510586097));
#106585=CARTESIAN_POINT('Ctrl Pts',(96.5391927502809,11.1445138219629,10.2576002197089));
#106586=CARTESIAN_POINT('Ctrl Pts',(96.7054282825438,11.5428021399452,10.2360493808081));
#106587=CARTESIAN_POINT('Ctrl Pts',(96.9918932170273,11.8141742722173,10.2144985419072));
#106588=CARTESIAN_POINT('Ctrl Pts',(97.3410933304653,12.1449762935684,10.1882281175622));
#106589=CARTESIAN_POINT('Ctrl Pts',(97.8689489900534,12.2871865058065,10.1619576932172));
#106590=CARTESIAN_POINT('Ctrl Pts',(98.3370695803043,12.1765798886882,10.1356872688721));
#106591=CARTESIAN_POINT('Ctrl Pts',(98.8051901705552,12.0659732715699,10.1094168445271));
#106592=CARTESIAN_POINT('Ctrl Pts',(99.2135756914689,11.7025498250952,10.0831464201821));
#106593=CARTESIAN_POINT('Ctrl Pts',(99.377790641522,11.2504390034582,10.0568759958371));
#106594=CARTESIAN_POINT('Ctrl Pts',(99.5420055915751,10.7983281818212,10.030605571492));
#106595=CARTESIAN_POINT('Ctrl Pts',(99.4620499707675,10.2575299850219,10.004335147147));
#106596=CARTESIAN_POINT('Ctrl Pts',(99.1740335407107,9.87228052451059,9.97806472280198));
#106597=CARTESIAN_POINT('Ctrl Pts',(98.8860171106538,9.4870310639993,9.95179429845695));
#106598=CARTESIAN_POINT('Ctrl Pts',(98.3899398713477,9.25733033977605,9.92552387411192));
#106599=CARTESIAN_POINT('Ctrl Pts',(97.9098404039135,9.28691530384111,9.89925344976689));
#106600=CARTESIAN_POINT('Ctrl Pts',(97.4297409364793,9.31650026790617,9.87298302542186));
#106601=CARTESIAN_POINT('Ctrl Pts',(96.965619240917,9.60537092025954,9.84671260107683));
#106602=CARTESIAN_POINT('Ctrl Pts',(96.7270829173316,10.0230686461859,9.8204421767318));
#106603=CARTESIAN_POINT('Ctrl Pts',(96.6021080103892,10.241910513299,9.8066784706911));
#106604=CARTESIAN_POINT('Ctrl Pts',(96.5390554685469,10.4961149441044,9.7929147646504));
#106605=CARTESIAN_POINT('Ctrl Pts',(96.5387662976346,10.750184760568,9.7791510586097));
#106606=CARTESIAN_POINT('Ctrl Pts',(96.5387723473756,10.7501752126031,9.70784096692389));
#106607=CARTESIAN_POINT('Ctrl Pts',(96.5390368470544,10.4969993434167,9.72155604363176));
#106608=CARTESIAN_POINT('Ctrl Pts',(96.6016181491467,10.2436988613999,9.73527112033962));
#106609=CARTESIAN_POINT('Ctrl Pts',(96.7257506472849,10.0254008549467,9.74898619704748));
#106610=CARTESIAN_POINT('Ctrl Pts',(96.9635191607655,9.60726383789951,9.77525662139251));
#106611=CARTESIAN_POINT('Ctrl Pts',(97.4271138034529,9.31754794143095,9.80152704573755));
#106612=CARTESIAN_POINT('Ctrl Pts',(97.9071590987782,9.28708417413698,9.82779747008257));
#106613=CARTESIAN_POINT('Ctrl Pts',(98.3872043941035,9.256620406843,9.8540678944276));
#106614=CARTESIAN_POINT('Ctrl Pts',(98.8837003420666,9.4854087687236,9.88033831877263));
#106615=CARTESIAN_POINT('Ctrl Pts',(99.1724221784704,9.87012895792189,9.90660874311765));
#106616=CARTESIAN_POINT('Ctrl Pts',(99.4611440148742,10.2548491471202,9.93287916746268));
#106617=CARTESIAN_POINT('Ctrl Pts',(99.5420917397186,10.7955011636361,9.95914959180771));
#106618=CARTESIAN_POINT('Ctrl Pts',(99.3787060978683,11.2479126394726,9.98542001615274));
#106619=CARTESIAN_POINT('Ctrl Pts',(99.215320456018,11.700324115309,10.0116904404978));
#106620=CARTESIAN_POINT('Ctrl Pts',(98.807601447473,12.0644950504659,10.0379608648428));
#106621=CARTESIAN_POINT('Ctrl Pts',(98.3396842729412,12.1759595319847,10.0642312891878));
#106622=CARTESIAN_POINT('Ctrl Pts',(97.8717670984094,12.2874240135035,10.0905017135329));
#106623=CARTESIAN_POINT('Ctrl Pts',(97.3436517578907,12.1461820413841,10.1167721378779));
#106624=CARTESIAN_POINT('Ctrl Pts',(96.9938457937009,11.8160208042116,10.1430425622229));
#106625=CARTESIAN_POINT('Ctrl Pts',(96.706236324123,11.5445631733553,10.1646420304566));
#106626=CARTESIAN_POINT('Ctrl Pts',(96.5391654491034,11.1453945765175,10.1862414986902));
#106627=CARTESIAN_POINT('Ctrl Pts',(96.5356817146954,10.7488128621349,10.2078409669239));
#106628=CARTESIAN_POINT('Origin',(98.,10.75,11.7549960127668));
#106629=CARTESIAN_POINT('',(96.5355008698795,10.7511408312974,10.7791510586097));
#106630=CARTESIAN_POINT('',(96.5355258561876,10.7511478400734,10.7078409669239));
#106631=CARTESIAN_POINT('',(96.5365,10.75,11.7549960127668));
#106632=CARTESIAN_POINT('Ctrl Pts',(96.5355008698795,10.7511408312974,10.7791510586097));
#106633=CARTESIAN_POINT('Ctrl Pts',(96.5348195355476,10.8305169224741,10.7748265234574));
#106634=CARTESIAN_POINT('Ctrl Pts',(96.5407253171912,10.9097915622436,10.7705019883051));
#106635=CARTESIAN_POINT('Ctrl Pts',(96.5535773406929,10.9879236072814,10.7661774531528));
#106636=CARTESIAN_POINT('Ctrl Pts',(96.631650035027,11.4625554245303,10.7399070288078));
#106637=CARTESIAN_POINT('Ctrl Pts',(96.966056138436,11.8950226859328,10.7136366044628));
#106638=CARTESIAN_POINT('Ctrl Pts',(97.4057708655159,12.0900141373515,10.6873661801177));
#106639=CARTESIAN_POINT('Ctrl Pts',(97.8454855925959,12.2850055887703,10.6610957557727));
#106640=CARTESIAN_POINT('Ctrl Pts',(98.3905089433467,12.2425212302052,10.6348253314277));
#106641=CARTESIAN_POINT('Ctrl Pts',(98.7946969823958,11.9817478870923,10.6085549070827));
#106642=CARTESIAN_POINT('Ctrl Pts',(99.198885021445,11.7209745439793,10.5822844827376));
#106643=CARTESIAN_POINT('Ctrl Pts',(99.4622377487925,11.2419122163185,10.5560140583926));
#106644=CARTESIAN_POINT('Ctrl Pts',(99.465819567919,10.7609154609234,10.5297436340476));
#106645=CARTESIAN_POINT('Ctrl Pts',(99.4694013870456,10.2799187055283,10.5034732097025));
#106646=CARTESIAN_POINT('Ctrl Pts',(99.2132122979512,9.796987522399,10.4772027853575));
#106647=CARTESIAN_POINT('Ctrl Pts',(98.812952649374,9.5302237317626,10.4509323610125));
#106648=CARTESIAN_POINT('Ctrl Pts',(98.4126930007967,9.2634599411262,10.4246619366675));
#106649=CARTESIAN_POINT('Ctrl Pts',(97.8683627927365,9.21286354298272,10.3983915123224));
#106650=CARTESIAN_POINT('Ctrl Pts',(97.4257929194293,9.40128491809413,10.3721210879774));
#106651=CARTESIAN_POINT('Ctrl Pts',(96.9832230461221,9.58970629320554,10.3458506636324));
#106652=CARTESIAN_POINT('Ctrl Pts',(96.6424135075679,10.0171454415718,10.3195802392873));
#106653=CARTESIAN_POINT('Ctrl Pts',(96.5572810219347,10.490561930987,10.2933098149423));
#106654=CARTESIAN_POINT('Ctrl Pts',(96.5419866348039,10.5756130722684,10.2885902294981));
#106655=CARTESIAN_POINT('Ctrl Pts',(96.534944362868,10.6621481571042,10.2838706440539));
#106656=CARTESIAN_POINT('Ctrl Pts',(96.5357076024386,10.7488070530836,10.2791510586097));
#106657=CARTESIAN_POINT('Ctrl Pts',(96.5356817146954,10.7488128621349,10.2078409669239));
#106658=CARTESIAN_POINT('Ctrl Pts',(96.5349283456612,10.6630507608455,10.2125119230353));
#106659=CARTESIAN_POINT('Ctrl Pts',(96.5418252088114,10.5774096363722,10.2171828791466));
#106660=CARTESIAN_POINT('Ctrl Pts',(96.5568076622876,10.4932072156605,10.221853835258));
#106661=CARTESIAN_POINT('Ctrl Pts',(96.6410720829249,10.0196353665074,10.248124259603));
#106662=CARTESIAN_POINT('Ctrl Pts',(96.9810975120607,9.59157217042678,10.2743946839481));
#106663=CARTESIAN_POINT('Ctrl Pts',(97.4233212663288,9.40233975759363,10.3006651082931));
#106664=CARTESIAN_POINT('Ctrl Pts',(97.8655450205969,9.21310734476048,10.3269355326381));
#106665=CARTESIAN_POINT('Ctrl Pts',(98.4099670999973,9.26270571517481,10.3532059569831));
#106666=CARTESIAN_POINT('Ctrl Pts',(98.8107151614298,9.52873528490133,10.3794763813282));
#106667=CARTESIAN_POINT('Ctrl Pts',(99.2114632228624,9.79476485462785,10.4057468056732));
#106668=CARTESIAN_POINT('Ctrl Pts',(99.4685372663271,10.2772256236666,10.4320172300182));
#106669=CARTESIAN_POINT('Ctrl Pts',(99.4658372583905,10.7582281877286,10.4582876543633));
#106670=CARTESIAN_POINT('Ctrl Pts',(99.4631372504539,11.2392307517907,10.4845580787083));
#106671=CARTESIAN_POINT('Ctrl Pts',(99.200663191116,11.7187751108762,10.5108285030533));
#106672=CARTESIAN_POINT('Ctrl Pts',(98.7969538623296,11.9802890289434,10.5370989273983));
#106673=CARTESIAN_POINT('Ctrl Pts',(98.3932445335432,12.2418029470106,10.5633693517434));
#106674=CARTESIAN_POINT('Ctrl Pts',(97.8482999353083,12.2852864240596,10.5896397760884));
#106675=CARTESIAN_POINT('Ctrl Pts',(97.4082284316461,12.0911014038513,10.6159102004334));
#106676=CARTESIAN_POINT('Ctrl Pts',(96.9681569279837,11.8969163836431,10.6421806247785));
#106677=CARTESIAN_POINT('Ctrl Pts',(96.632958518894,11.4650628661776,10.6684510491235));
#106678=CARTESIAN_POINT('Ctrl Pts',(96.5540158140872,10.9905749299596,10.6947214734685));
#106679=CARTESIAN_POINT('Ctrl Pts',(96.5408744415503,10.9115882427239,10.6990946379536));
#106680=CARTESIAN_POINT('Ctrl Pts',(96.5348342566888,10.8314200988262,10.7034678024388));
#106681=CARTESIAN_POINT('Ctrl Pts',(96.5355258561876,10.7511478400734,10.7078409669239));
#106682=CARTESIAN_POINT('Origin',(98.,10.75,11.7549960127668));
#106683=CARTESIAN_POINT('',(96.5387850105563,10.7499314378747,11.2791510586097));
#106684=CARTESIAN_POINT('',(96.5387834722467,10.7499171729064,11.2078409669239));
#106685=CARTESIAN_POINT('',(96.5365,10.75,11.7549960127668));
#106686=CARTESIAN_POINT('Ctrl Pts',(96.5387850105563,10.7499314378747,11.2791510586097));
#106687=CARTESIAN_POINT('Ctrl Pts',(96.5388896036327,10.9967165449052,11.2657824028609));
#106688=CARTESIAN_POINT('Ctrl Pts',(96.5981895170845,11.2435488522249,11.2524137471121));
#106689=CARTESIAN_POINT('Ctrl Pts',(96.7163984162244,11.4578934427831,11.2390450913634));
#106690=CARTESIAN_POINT('Ctrl Pts',(96.9486878849727,11.8790968499048,11.2127746670183));
#106691=CARTESIAN_POINT('Ctrl Pts',(97.4084557934653,12.1748481713484,11.1865042426733));
#106692=CARTESIAN_POINT('Ctrl Pts',(97.8880613453677,12.2115799293275,11.1602338183283));
#106693=CARTESIAN_POINT('Ctrl Pts',(98.3676668972702,12.2483116873066,11.1339633939832));
#106694=CARTESIAN_POINT('Ctrl Pts',(98.8671100925825,12.0260238818212,11.1076929696382));
#106695=CARTESIAN_POINT('Ctrl Pts',(99.1608319462644,11.6451063315194,11.0814225452932));
#106696=CARTESIAN_POINT('Ctrl Pts',(99.4545537999463,11.2641887812175,11.0551521209481));
#106697=CARTESIAN_POINT('Ctrl Pts',(99.5425543119979,10.7246414860992,11.0288816966031));
#106698=CARTESIAN_POINT('Ctrl Pts',(99.3850906120084,10.2701352807983,11.0026112722581));
#106699=CARTESIAN_POINT('Ctrl Pts',(99.2276269120188,9.8156290754975,10.9763408479131));
#106700=CARTESIAN_POINT('Ctrl Pts',(98.8246989999881,9.44616396001416,10.950070423568));
#106701=CARTESIAN_POINT('Ctrl Pts',(98.3582775419532,9.3285981021577,10.923799999223));
#106702=CARTESIAN_POINT('Ctrl Pts',(97.8918560839184,9.21103224430123,10.897529574878));
#106703=CARTESIAN_POINT('Ctrl Pts',(97.3619410798795,9.34536564407164,10.8712591505329));
#106704=CARTESIAN_POINT('Ctrl Pts',(97.0078532204896,9.67093053050446,10.8449887261879));
#106705=CARTESIAN_POINT('Ctrl Pts',(96.7120539283044,9.94290219068257,10.8230428369952));
#106706=CARTESIAN_POINT('Ctrl Pts',(96.5389584641005,10.3483278490524,10.8010969478024));
#106707=CARTESIAN_POINT('Ctrl Pts',(96.5355008698795,10.7511408312974,10.7791510586097));
#106708=CARTESIAN_POINT('Ctrl Pts',(96.5355258561876,10.7511478400734,10.7078409669239));
#106709=CARTESIAN_POINT('Ctrl Pts',(96.5389888253935,10.3492094918976,10.7297382267838));
#106710=CARTESIAN_POINT('Ctrl Pts',(96.7112306802982,9.94466078244129,10.7516354866437));
#106711=CARTESIAN_POINT('Ctrl Pts',(97.005876554875,9.67275112583176,10.7735327465036));
#106712=CARTESIAN_POINT('Ctrl Pts',(97.3593670009933,9.34653761289245,10.7998031708486));
#106713=CARTESIAN_POINT('Ctrl Pts',(97.8890348937537,9.21123294198437,10.8260735951937));
#106714=CARTESIAN_POINT('Ctrl Pts',(98.3556711437306,9.32794353138054,10.8523440195387));
#106715=CARTESIAN_POINT('Ctrl Pts',(98.8223073937075,9.44465412077671,10.8786144438837));
#106716=CARTESIAN_POINT('Ctrl Pts',(99.2259120009009,9.81337997047714,10.9048848682287));
#106717=CARTESIAN_POINT('Ctrl Pts',(99.3842086892949,10.2675967800744,10.9311552925738));
#106718=CARTESIAN_POINT('Ctrl Pts',(99.5425053776888,10.7218135896718,10.9574257169188));
#106719=CARTESIAN_POINT('Ctrl Pts',(99.4554941472833,11.2615213591659,10.9836961412638));
#106720=CARTESIAN_POINT('Ctrl Pts',(99.1624710883709,11.6429767805759,11.0099665656089));
#106721=CARTESIAN_POINT('Ctrl Pts',(98.8694480294585,12.0244322019858,11.0362369899539));
#106722=CARTESIAN_POINT('Ctrl Pts',(98.3704131420392,12.2476352753116,11.0625074142989));
#106723=CARTESIAN_POINT('Ctrl Pts',(97.8907410107022,12.211782827704,11.0887778386439));
#106724=CARTESIAN_POINT('Ctrl Pts',(97.4110688793651,12.1759303800964,11.115048262989));
#106725=CARTESIAN_POINT('Ctrl Pts',(96.9507595041103,11.8810224115554,11.141318687334));
#106726=CARTESIAN_POINT('Ctrl Pts',(96.7176982190144,11.4602455241283,11.167589111679));
#106727=CARTESIAN_POINT('Ctrl Pts',(96.5986651321274,11.2453390810417,11.1810063967606));
#106728=CARTESIAN_POINT('Ctrl Pts',(96.5389102934636,10.9975994070483,11.1944236818423));
#106729=CARTESIAN_POINT('Ctrl Pts',(96.5387834722467,10.7499171729064,11.2078409669239));
#106730=CARTESIAN_POINT('Origin',(98.,10.75,11.7549960127668));
#106731=CARTESIAN_POINT('',(96.5352653497957,10.7489347653901,11.7791510586097));
#106732=CARTESIAN_POINT('',(96.5352413523044,10.7489434884042,11.7078409669239));
#106733=CARTESIAN_POINT('',(96.5365,10.75,11.7549960127668));
#106734=CARTESIAN_POINT('Ctrl Pts',(96.5352653497957,10.7489347653901,11.7791510586097));
#106735=CARTESIAN_POINT('Ctrl Pts',(96.5386412990586,11.1601452319407,11.7567382822644));
#106736=CARTESIAN_POINT('Ctrl Pts',(96.7200647749387,11.5739666593434,11.7343255059191));
#106737=CARTESIAN_POINT('Ctrl Pts',(97.0269988720097,11.8463644271576,11.7119127295739));
#106738=CARTESIAN_POINT('Ctrl Pts',(97.3867619308914,12.1656468239869,11.6856423052288));
#106739=CARTESIAN_POINT('Ctrl Pts',(97.9189591634772,12.290632740949,11.6593718808838));
#106740=CARTESIAN_POINT('Ctrl Pts',(98.3832391769487,12.1648759258178,11.6331014565388));
#106741=CARTESIAN_POINT('Ctrl Pts',(98.8475191904202,12.0391191106867,11.6068310321937));
#106742=CARTESIAN_POINT('Ctrl Pts',(99.2438819847773,11.6626195634623,11.5805606078487));
#106743=CARTESIAN_POINT('Ctrl Pts',(99.3933218383592,11.2054123482717,11.5542901835037));
#106744=CARTESIAN_POINT('Ctrl Pts',(99.5427616919411,10.7482051330811,11.5280197591587));
#106745=CARTESIAN_POINT('Ctrl Pts',(99.4452786047477,10.2102902499242,11.5017493348136));
#106746=CARTESIAN_POINT('Ctrl Pts',(99.1448979762896,9.834601302112,11.4754789104686));
#106747=CARTESIAN_POINT('Ctrl Pts',(98.8445173478316,9.45891235429976,11.4492084861236));
#106748=CARTESIAN_POINT('Ctrl Pts',(98.3412391781088,9.24544934183213,11.4229380617785));
#106749=CARTESIAN_POINT('Ctrl Pts',(97.8623544067611,9.29061662238126,11.3966676374335));
#106750=CARTESIAN_POINT('Ctrl Pts',(97.3834696354134,9.33578390293038,11.3703972130885));
#106751=CARTESIAN_POINT('Ctrl Pts',(96.9289782624408,9.63958147649625,11.3441267887435));
#106752=CARTESIAN_POINT('Ctrl Pts',(96.7041380904565,10.064808009679,11.3178563643984));
#106753=CARTESIAN_POINT('Ctrl Pts',(96.5937159734788,10.2736426390726,11.3049545958022));
#106754=CARTESIAN_POINT('Ctrl Pts',(96.5386840702901,10.511765057968,11.292052827206));
#106755=CARTESIAN_POINT('Ctrl Pts',(96.5387850105563,10.7499314378747,11.2791510586097));
#106756=CARTESIAN_POINT('Ctrl Pts',(96.5387834722467,10.7499171729064,11.2078409669239));
#106757=CARTESIAN_POINT('Ctrl Pts',(96.5386619833798,10.5126490348939,11.2206941061873));
#106758=CARTESIAN_POINT('Ctrl Pts',(96.5932596645075,10.2754336080251,11.2335472454507));
#106759=CARTESIAN_POINT('Ctrl Pts',(96.7028839945097,10.067184775836,11.2464003847141));
#106760=CARTESIAN_POINT('Ctrl Pts',(96.9269442500378,9.64154672128373,11.2726708090591));
#106761=CARTESIAN_POINT('Ctrl Pts',(97.3808779560309,9.33691641849236,11.2989412334042));
#106762=CARTESIAN_POINT('Ctrl Pts',(97.8596791639475,9.29087127879738,11.3252116577492));
#106763=CARTESIAN_POINT('Ctrl Pts',(98.3384803718641,9.24482613910239,11.3514820820942));
#106764=CARTESIAN_POINT('Ctrl Pts',(98.8421490817041,9.45736616250379,11.3777525064392));
#106765=CARTESIAN_POINT('Ctrl Pts',(99.1432179777445,9.83250383247476,11.4040229307843));
#106766=CARTESIAN_POINT('Ctrl Pts',(99.4442868737849,10.2076415024457,11.4302933551293));
#106767=CARTESIAN_POINT('Ctrl Pts',(99.5427559560256,10.7453768189863,11.4565637794743));
#106768=CARTESIAN_POINT('Ctrl Pts',(99.3941545289882,11.2028572748257,11.4828342038194));
#106769=CARTESIAN_POINT('Ctrl Pts',(99.2455531019507,11.6603377306651,11.5091046281644));
#106770=CARTESIAN_POINT('Ctrl Pts',(98.8498811656352,12.0375633258033,11.5353750525094));
#106771=CARTESIAN_POINT('Ctrl Pts',(98.3858324357713,12.1641710976999,11.5616454768544));
#106772=CARTESIAN_POINT('Ctrl Pts',(97.9217837059074,12.2907788695965,11.5879159011995));
#106773=CARTESIAN_POINT('Ctrl Pts',(97.3893581824952,12.1667688182515,11.6141863255445));
#106774=CARTESIAN_POINT('Ctrl Pts',(97.0290103592619,11.848146474584,11.6404567498895));
#106775=CARTESIAN_POINT('Ctrl Pts',(96.7209103249204,11.575722031597,11.6629181555677));
#106776=CARTESIAN_POINT('Ctrl Pts',(96.5386055516053,11.1610286944639,11.6853795612458));
#106777=CARTESIAN_POINT('Ctrl Pts',(96.5352413523044,10.7489434884042,11.7078409669239));
#106778=CARTESIAN_POINT('Origin',(98.,10.75,11.7549960127668));
#106779=CARTESIAN_POINT('',(96.5359578915487,10.751240120072,12.2791510586097));
#106780=CARTESIAN_POINT('',(96.5359840746412,10.7512441236452,12.2078409669239));
#106781=CARTESIAN_POINT('',(96.5365,10.75,11.7549960127668));
#106782=CARTESIAN_POINT('Ctrl Pts',(96.5359578915487,10.751240120072,12.2791510586097));
#106783=CARTESIAN_POINT('Ctrl Pts',(96.5351035673496,10.8465138711225,12.273964586013));
#106784=CARTESIAN_POINT('Ctrl Pts',(96.5436208912905,10.941635625592,12.2687781134162));
#106785=CARTESIAN_POINT('Ctrl Pts',(96.5620706913964,11.034790195851,12.2635916408195));
#106786=CARTESIAN_POINT('Ctrl Pts',(96.6555222750729,11.5066349891535,12.2373212164744));
#106787=CARTESIAN_POINT('Ctrl Pts',(97.0038020855935,11.9280095818795,12.2110507921294));
#106788=CARTESIAN_POINT('Ctrl Pts',(97.4496196817153,12.1086124014813,12.1847803677844));
#106789=CARTESIAN_POINT('Ctrl Pts',(97.8954372778371,12.289215221083,12.1585099434393));
#106790=CARTESIAN_POINT('Ctrl Pts',(98.43879265956,12.2290462675604,12.1322395190943));
#106791=CARTESIAN_POINT('Ctrl Pts',(98.8342951807105,11.9552790978233,12.1059690947493));
#106792=CARTESIAN_POINT('Ctrl Pts',(99.2297977018609,11.6815119280863,12.0796986704043));
#106793=CARTESIAN_POINT('Ctrl Pts',(99.477447362439,11.1941465421347,12.0534282460592));
#106794=CARTESIAN_POINT('Ctrl Pts',(99.4654004000111,10.7132873338868,12.0271578217142));
#106795=CARTESIAN_POINT('Ctrl Pts',(99.4533534375832,10.2324281256388,12.0008873973692));
#106796=CARTESIAN_POINT('Ctrl Pts',(99.1816098521493,9.75807509509448,11.9746169730242));
#106797=CARTESIAN_POINT('Ctrl Pts',(98.7728947261572,9.5044559845247,11.9483465486791));
#106798=CARTESIAN_POINT('Ctrl Pts',(98.3641796001652,9.25083687395492,11.9220761243341));
#106799=CARTESIAN_POINT('Ctrl Pts',(97.8184929336149,9.21795168335968,11.8958056999891));
#106800=CARTESIAN_POINT('Ctrl Pts',(97.3822782296244,9.42065205209055,11.869535275644));
#106801=CARTESIAN_POINT('Ctrl Pts',(96.9460635256339,9.62335242082142,11.843264851299));
#106802=CARTESIAN_POINT('Ctrl Pts',(96.6193207842032,10.0616383488784,11.816994426954));
#106803=CARTESIAN_POINT('Ctrl Pts',(96.5496138560767,10.5375707512551,11.790724002609));
#106804=CARTESIAN_POINT('Ctrl Pts',(96.5393778283551,10.6074584567573,11.7868663546092));
#106805=CARTESIAN_POINT('Ctrl Pts',(96.5346842872928,10.6781579366151,11.7830087066095));
#106806=CARTESIAN_POINT('Ctrl Pts',(96.5352653497957,10.7489347653901,11.7791510586097));
#106807=CARTESIAN_POINT('Ctrl Pts',(96.5352413523044,10.7489434884042,11.7078409669239));
#106808=CARTESIAN_POINT('Ctrl Pts',(96.5346708493661,10.6790618316311,11.7116499855908));
#106809=CARTESIAN_POINT('Ctrl Pts',(96.5392462443228,10.6092551783963,11.7154590042577));
#106810=CARTESIAN_POINT('Ctrl Pts',(96.5492267123949,10.5402300545035,11.7192680229246));
#106811=CARTESIAN_POINT('Ctrl Pts',(96.6180610118158,10.0641706140802,11.7455384472697));
#106812=CARTESIAN_POINT('Ctrl Pts',(96.943999733712,9.62528636922334,11.7718088716147));
#106813=CARTESIAN_POINT('Ctrl Pts',(97.3798421393641,9.42178661731112,11.7980792959597));
#106814=CARTESIAN_POINT('Ctrl Pts',(97.8156845450163,9.21828686539889,11.8243497203047));
#106815=CARTESIAN_POINT('Ctrl Pts',(98.3614306344244,9.25017160643128,11.8506201446498));
#106816=CARTESIAN_POINT('Ctrl Pts',(98.7706100678667,9.5030410249873,11.8768905689948));
#106817=CARTESIAN_POINT('Ctrl Pts',(99.179789501309,9.75591044354332,11.9031609933398));
#106818=CARTESIAN_POINT('Ctrl Pts',(99.4524022787855,10.229764539623,11.9294314176849));
#106819=CARTESIAN_POINT('Ctrl Pts',(99.4653307725548,10.7106009001884,11.9557018420299));
#106820=CARTESIAN_POINT('Ctrl Pts',(99.4782592663242,11.1914372607538,11.9819722663749));
#106821=CARTESIAN_POINT('Ctrl Pts',(99.2315034763865,11.6792558858049,12.0082426907199));
#106822=CARTESIAN_POINT('Ctrl Pts',(98.8365034745158,11.9537476891712,12.034513115065));
#106823=CARTESIAN_POINT('Ctrl Pts',(98.4415034726451,12.2282394925375,12.06078353941));
#106824=CARTESIAN_POINT('Ctrl Pts',(97.8982592588414,12.2894044742189,12.087053963755));
#106825=CARTESIAN_POINT('Ctrl Pts',(97.4521112735164,12.1096192501782,12.1133243881001));
#106826=CARTESIAN_POINT('Ctrl Pts',(97.0059632881914,11.9298340261375,12.1395948124451));
#106827=CARTESIAN_POINT('Ctrl Pts',(96.6569115313452,11.5090985963747,12.1658652367901));
#106828=CARTESIAN_POINT('Ctrl Pts',(96.562595071327,11.0374258740744,12.1921356611351));
#106829=CARTESIAN_POINT('Ctrl Pts',(96.5437999321489,10.9434321590808,12.1973707630647));
#106830=CARTESIAN_POINT('Ctrl Pts',(96.5351207094314,10.8474156486503,12.2026058649943));
#106831=CARTESIAN_POINT('Ctrl Pts',(96.5359840746412,10.7512441236452,12.2078409669239));
#106832=CARTESIAN_POINT('Origin',(98.,10.75,11.7549960127668));
#106833=CARTESIAN_POINT('',(96.5387213242412,10.7496813739491,12.7791510586097));
#106834=CARTESIAN_POINT('',(96.5387151545458,10.7496675338344,12.7078409669239));
#106835=CARTESIAN_POINT('',(96.5365,10.75,11.7549960127668));
#106836=CARTESIAN_POINT('Ctrl Pts',(96.5387213242412,10.7496813739491,12.7791510586097));
#106837=CARTESIAN_POINT('Ctrl Pts',(96.5392400434179,11.0123491908163,12.7649204654165));
#106838=CARTESIAN_POINT('Ctrl Pts',(96.6068977921477,11.2752662571728,12.7506898722232));
#106839=CARTESIAN_POINT('Ctrl Pts',(96.7400744574238,11.4992221154966,12.73645927903));
#106840=CARTESIAN_POINT('Ctrl Pts',(96.9859255939258,11.9126564223331,12.7101888546849));
#106841=CARTESIAN_POINT('Ctrl Pts',(97.4550593278255,12.1933144229382,12.6839184303399));
#106842=CARTESIAN_POINT('Ctrl Pts',(97.9356050612555,12.2144450977881,12.6576480059949));
#106843=CARTESIAN_POINT('Ctrl Pts',(98.4161507946855,12.2355757726381,12.6313775816499));
#106844=CARTESIAN_POINT('Ctrl Pts',(98.9081085276457,11.9971791217329,12.6051071573048));
#106845=CARTESIAN_POINT('Ctrl Pts',(99.1892998658561,11.6069200553923,12.5788367329598));
#106846=CARTESIAN_POINT('Ctrl Pts',(99.4704912040665,11.2166609890518,12.5525663086148));
#106847=CARTESIAN_POINT('Ctrl Pts',(99.540916147527,10.6745395072759,12.5262958842698));
#106848=CARTESIAN_POINT('Ctrl Pts',(99.3687693201679,10.2253890010137,12.5000254599247));
#106849=CARTESIAN_POINT('Ctrl Pts',(99.1966224928088,9.77623849475159,12.4737550355797));
#106850=CARTESIAN_POINT('Ctrl Pts',(98.7819038946301,9.42005896400319,12.4474846112347));
#106851=CARTESIAN_POINT('Ctrl Pts',(98.311909111808,9.31770852888495,12.4212141868896));
#106852=CARTESIAN_POINT('Ctrl Pts',(97.841914328986,9.21535809376671,12.3949437625446));
#106853=CARTESIAN_POINT('Ctrl Pts',(97.3166433615205,9.36683675427863,12.3686733381996));
#106854=CARTESIAN_POINT('Ctrl Pts',(96.973319556204,9.70373358147408,12.3424029138545));
#106855=CARTESIAN_POINT('Ctrl Pts',(96.6977768984129,9.97411811563489,12.3213189621063));
#106856=CARTESIAN_POINT('Ctrl Pts',(96.5394308743624,10.3639350427664,12.300235010358));
#106857=CARTESIAN_POINT('Ctrl Pts',(96.5359578915487,10.751240120072,12.2791510586097));
#106858=CARTESIAN_POINT('Ctrl Pts',(96.5359840746412,10.7512441236452,12.2078409669239));
#106859=CARTESIAN_POINT('Ctrl Pts',(96.5394531886708,10.3648143916403,12.2288762893393));
#106860=CARTESIAN_POINT('Ctrl Pts',(96.6969909367875,9.97588189162702,12.2499116117548));
#106861=CARTESIAN_POINT('Ctrl Pts',(96.9714030824048,9.70561743447366,12.2709469341702));
#106862=CARTESIAN_POINT('Ctrl Pts',(97.3141087166909,9.36809173201119,12.2972173585153));
#106863=CARTESIAN_POINT('Ctrl Pts',(97.8391011484532,9.21565034192411,12.3234877828603));
#106864=CARTESIAN_POINT('Ctrl Pts',(98.3092828234955,9.31713898191082,12.3497582072053));
#106865=CARTESIAN_POINT('Ctrl Pts',(98.7794644985377,9.41862762189754,12.3760286315503));
#106866=CARTESIAN_POINT('Ctrl Pts',(99.1948354168599,9.77404629195804,12.4022990558954));
#106867=CARTESIAN_POINT('Ctrl Pts',(99.3678053907722,10.2228804926548,12.4285694802404));
#106868=CARTESIAN_POINT('Ctrl Pts',(99.5407753646844,10.6717146933516,12.4548399045854));
#106869=CARTESIAN_POINT('Ctrl Pts',(99.4713443941867,11.2139644246847,12.4811103289305));
#106870=CARTESIAN_POINT('Ctrl Pts',(99.1908689565956,11.6047383753408,12.5073807532755));
#106871=CARTESIAN_POINT('Ctrl Pts',(98.9103935190044,11.9955123259969,12.5336511776205));
#106872=CARTESIAN_POINT('Ctrl Pts',(98.4188736143198,12.234810495976,12.5599216019655));
#106873=CARTESIAN_POINT('Ctrl Pts',(97.9382899039966,12.2145608304758,12.5861920263106));
#106874=CARTESIAN_POINT('Ctrl Pts',(97.4577061936734,12.1943111649755,12.6124624506556));
#106875=CARTESIAN_POINT('Ctrl Pts',(96.9880586777116,11.9145136639958,12.6387328750006));
#106876=CARTESIAN_POINT('Ctrl Pts',(96.7414499895577,11.5015307266915,12.6650032993457));
#106877=CARTESIAN_POINT('Ctrl Pts',(96.607406462557,11.277054898521,12.6792825218717));
#106878=CARTESIAN_POINT('Ctrl Pts',(96.5392583845217,11.0132302528889,12.6935617443978));
#106879=CARTESIAN_POINT('Ctrl Pts',(96.5387151545458,10.7496675338344,12.7078409669239));
#106880=CARTESIAN_POINT('Origin',(98.,10.75,11.7549960127668));
#106881=CARTESIAN_POINT('',(96.5348664968456,10.7491119138617,13.2791510586097));
#106882=CARTESIAN_POINT('',(96.5348456374124,10.749123229052,13.2078409669239));
#106883=CARTESIAN_POINT('',(96.5365,10.75,11.7549960127668));
#106884=CARTESIAN_POINT('Ctrl Pts',(96.5348664968456,10.7491119138617,13.2791510586097));
#106885=CARTESIAN_POINT('Ctrl Pts',(96.5379355734796,11.175832275792,13.25587634482));
#106886=CARTESIAN_POINT('Ctrl Pts',(96.7353719317325,11.6050282494574,13.2326016310302));
#106887=CARTESIAN_POINT('Ctrl Pts',(97.0631318295525,11.8773970516098,13.2093269172405));
#106888=CARTESIAN_POINT('Ctrl Pts',(97.4330780156496,12.1848227014171,13.1830564928955));
#106889=CARTESIAN_POINT('Ctrl Pts',(97.9690548809394,12.292452352062,13.1567860685504));
#106890=CARTESIAN_POINT('Ctrl Pts',(98.4290041376041,12.1516781433137,13.1305156442054));
#106891=CARTESIAN_POINT('Ctrl Pts',(98.8889533942687,12.0109039345654,13.1042452198604));
#106892=CARTESIAN_POINT('Ctrl Pts',(99.2728750423081,11.621725866424,13.0779747955154));
#106893=CARTESIAN_POINT('Ctrl Pts',(99.4073820091069,11.1599049179571,13.0517043711703));
#106894=CARTESIAN_POINT('Ctrl Pts',(99.5418889759057,10.6980839694902,13.0254339468253));
#106895=CARTESIAN_POINT('Ctrl Pts',(99.4269812614638,10.1636201406978,12.9991635224803));
#106896=CARTESIAN_POINT('Ctrl Pts',(99.1145536072369,9.79788845184339,12.9728930981352));
#106897=CARTESIAN_POINT('Ctrl Pts',(98.8021259530099,9.43215676298898,12.9466226737902));
#106898=CARTESIAN_POINT('Ctrl Pts',(98.2921783589979,9.23515721407256,12.9203522494452));
#106899=CARTESIAN_POINT('Ctrl Pts',(97.8150138082797,9.29585892584242,12.8940818251001));
#106900=CARTESIAN_POINT('Ctrl Pts',(97.3378492575615,9.35656063761229,12.8678114007551));
#106901=CARTESIAN_POINT('Ctrl Pts',(96.8934677501372,9.67496361006843,12.8415409764101));
#106902=CARTESIAN_POINT('Ctrl Pts',(96.6825612659772,10.1072704028304,12.8152705520651));
#106903=CARTESIAN_POINT('Ctrl Pts',(96.5859020561848,10.3053981803746,12.8032307209133));
#106904=CARTESIAN_POINT('Ctrl Pts',(96.5382824605045,10.5274505701347,12.7911908897615));
#106905=CARTESIAN_POINT('Ctrl Pts',(96.5387213242412,10.7496813739491,12.7791510586097));
#106906=CARTESIAN_POINT('Ctrl Pts',(96.5387151545458,10.7496675338344,12.7078409669239));
#106907=CARTESIAN_POINT('Ctrl Pts',(96.5382589686252,10.5283365929963,12.7198321687428));
#106908=CARTESIAN_POINT('Ctrl Pts',(96.5854781604418,10.3071903644812,12.7318233705618));
#106909=CARTESIAN_POINT('Ctrl Pts',(96.6813850502399,10.1096866576566,12.7438145723807));
#106910=CARTESIAN_POINT('Ctrl Pts',(96.8914986594218,9.6769938995548,12.7700849967258));
#106911=CARTESIAN_POINT('Ctrl Pts',(97.3352957381316,9.35777675697994,12.7963554210708));
#106912=CARTESIAN_POINT('Ctrl Pts',(97.812348250158,9.29620036345914,12.8226258454158));
#106913=CARTESIAN_POINT('Ctrl Pts',(98.2894007621844,9.23462396993834,12.8488962697608));
#106914=CARTESIAN_POINT('Ctrl Pts',(98.7997087075274,9.43068832547161,12.8751666941059));
#106915=CARTESIAN_POINT('Ctrl Pts',(99.1128063537502,9.79584666845564,12.9014371184509));
#106916=CARTESIAN_POINT('Ctrl Pts',(99.425903999973,10.1610050114397,12.9277075427959));
#106917=CARTESIAN_POINT('Ctrl Pts',(99.5417913470757,10.6952573418744,12.953977967141));
#106918=CARTESIAN_POINT('Ctrl Pts',(99.4081312455337,11.1573241438787,12.980248391486));
#106919=CARTESIAN_POINT('Ctrl Pts',(99.2744711439917,11.6193909458829,13.006518815831));
#106920=CARTESIAN_POINT('Ctrl Pts',(98.8912635938049,12.0092722194565,13.032789240176));
#106921=CARTESIAN_POINT('Ctrl Pts',(98.4315731366753,12.1508894289787,13.0590596645211));
#106922=CARTESIAN_POINT('Ctrl Pts',(97.9718826795457,12.2925066385009,13.0853300888661));
#106923=CARTESIAN_POINT('Ctrl Pts',(97.4357093154733,12.1858597839718,13.1116005132111));
#106924=CARTESIAN_POINT('Ctrl Pts',(97.0652001347814,11.8791128222671,13.1378709375562));
#106925=CARTESIAN_POINT('Ctrl Pts',(96.7362555909916,11.6067774939266,13.1611942806787));
#106926=CARTESIAN_POINT('Ctrl Pts',(96.5378908628165,11.1767192675748,13.1845176238013));
#106927=CARTESIAN_POINT('Ctrl Pts',(96.5348456374124,10.749123229052,13.2078409669239));
#106928=CARTESIAN_POINT('Origin',(98.,10.75,11.7549960127668));
#106929=CARTESIAN_POINT('',(96.5364271352644,10.7512852130388,13.7791510586097));
#106930=CARTESIAN_POINT('',(96.5364532332071,10.7512863178753,13.7078409669239));
#106931=CARTESIAN_POINT('',(96.5365,10.75,11.7549960127668));
#106932=CARTESIAN_POINT('Ctrl Pts',(96.5364271352644,10.7512852130388,13.7791510586097));
#106933=CARTESIAN_POINT('Ctrl Pts',(96.5354273092983,10.8624851060287,13.7731026485685));
#106934=CARTESIAN_POINT('Ctrl Pts',(96.5470462255384,10.9734783641957,13.7670542385273));
#106935=CARTESIAN_POINT('Ctrl Pts',(96.5720796503353,11.0813584317053,13.7610058284861));
#106936=CARTESIAN_POINT('Ctrl Pts',(96.6808088349878,11.5499204393302,13.7347354041411));
#106937=CARTESIAN_POINT('Ctrl Pts',(97.0425997605388,11.959752792851,13.708464979796));
#106938=CARTESIAN_POINT('Ctrl Pts',(97.4940508333205,12.1257751154429,13.682194555451));
#106939=CARTESIAN_POINT('Ctrl Pts',(97.9455019061022,12.2917974380347,13.655924131106));
#106940=CARTESIAN_POINT('Ctrl Pts',(98.4866131261147,12.2140097296976,13.6296537067609));
#106941=CARTESIAN_POINT('Ctrl Pts',(98.8730119243886,11.9275383591108,13.6033832824159));
#106942=CARTESIAN_POINT('Ctrl Pts',(99.2594107226625,11.6410669885239,13.5771128580709));
#106943=CARTESIAN_POINT('Ctrl Pts',(99.4910970991978,11.1459119556874,13.5508424337259));
#106944=CARTESIAN_POINT('Ctrl Pts',(99.4634343896403,10.6656976884966,13.5245720093808));
#106945=CARTESIAN_POINT('Ctrl Pts',(99.4357716800828,10.1854834213057,13.4983015850358));
#106946=CARTESIAN_POINT('Ctrl Pts',(99.1487598844324,9.72020991976056,13.4720311606908));
#106947=CARTESIAN_POINT('Ctrl Pts',(98.7320206410468,9.48000340079889,13.4457607363457));
#106948=CARTESIAN_POINT('Ctrl Pts',(98.3152813976611,9.23979688183723,13.4194903120007));
#106949=CARTESIAN_POINT('Ctrl Pts',(97.7688147065403,9.22465734545908,13.3932198876557));
#106950=CARTESIAN_POINT('Ctrl Pts',(97.3394157966844,9.44142262640037,13.3669494633107));
#106951=CARTESIAN_POINT('Ctrl Pts',(96.9100168868285,9.65818790734167,13.3406790389656));
#106952=CARTESIAN_POINT('Ctrl Pts',(96.5976857582377,10.1068580056024,13.3144086146206));
#106953=CARTESIAN_POINT('Ctrl Pts',(96.5434779473944,10.5848038792176,13.2881381902756));
#106954=CARTESIAN_POINT('Ctrl Pts',(96.5372964366206,10.6393057585798,13.2851424797203));
#106955=CARTESIAN_POINT('Ctrl Pts',(96.5344714730721,10.6941883300987,13.282146769165));
#106956=CARTESIAN_POINT('Ctrl Pts',(96.5348664968456,10.7491119138617,13.2791510586097));
#106957=CARTESIAN_POINT('Ctrl Pts',(96.5348456374124,10.749123229052,13.2078409669239));
#106958=CARTESIAN_POINT('Ctrl Pts',(96.5344608500961,10.6950932278937,13.2107880481463));
#106959=CARTESIAN_POINT('Ctrl Pts',(96.5371945805109,10.6411025386132,13.2137351293688));
#106960=CARTESIAN_POINT('Ctrl Pts',(96.5431774380789,10.5874743274537,13.2166822105912));
#106961=CARTESIAN_POINT('Ctrl Pts',(96.5965089193795,10.1094298632253,13.2429526349363));
#106962=CARTESIAN_POINT('Ctrl Pts',(96.9080168792921,9.66018800364869,13.2692230592813));
#106963=CARTESIAN_POINT('Ctrl Pts',(97.337017785826,9.4426357963421,13.2954934836263));
#106964=CARTESIAN_POINT('Ctrl Pts',(97.7660186923598,9.22508358903551,13.3217639079714));
#106965=CARTESIAN_POINT('Ctrl Pts',(98.3125125455149,9.23922103399892,13.3480343323164));
#106966=CARTESIAN_POINT('Ctrl Pts',(98.7296913544854,9.47866329478746,13.3743047566614));
#106967=CARTESIAN_POINT('Ctrl Pts',(99.1468701634559,9.71810555557601,13.4005751810064));
#106968=CARTESIAN_POINT('Ctrl Pts',(99.4347339282419,10.1828526321897,13.4268456053515));
#106969=CARTESIAN_POINT('Ctrl Pts',(99.4632772457784,10.6630151754182,13.4531160296965));
#106970=CARTESIAN_POINT('Ctrl Pts',(99.4918205633151,11.1431777186466,13.4793864540415));
#106971=CARTESIAN_POINT('Ctrl Pts',(99.2610434336023,11.6387557284899,13.5056568783866));
#106972=CARTESIAN_POINT('Ctrl Pts',(98.8751698558169,11.9259355277118,13.5319273027316));
#106973=CARTESIAN_POINT('Ctrl Pts',(98.4892962780315,12.2131153269336,13.5581977270766));
#106974=CARTESIAN_POINT('Ctrl Pts',(97.9483262521734,12.2918969155339,13.5844681514217));
#106975=CARTESIAN_POINT('Ctrl Pts',(97.4965726934334,12.1267014705973,13.6107385757667));
#106976=CARTESIAN_POINT('Ctrl Pts',(97.0448191346934,11.9615060256606,13.6370090001117));
#106977=CARTESIAN_POINT('Ctrl Pts',(96.6822820430715,11.552333547187,13.6632794244567));
#106978=CARTESIAN_POINT('Ctrl Pts',(96.5726916665336,11.0839736846863,13.6895498488018));
#106979=CARTESIAN_POINT('Ctrl Pts',(96.5472571005748,10.9752731747371,13.6956468881758));
#106980=CARTESIAN_POINT('Ctrl Pts',(96.5354474203,10.8633845572015,13.7017439275498));
#106981=CARTESIAN_POINT('Ctrl Pts',(96.5364532332071,10.7512863178753,13.7078409669239));
#106982=CARTESIAN_POINT('Origin',(98.,10.75,11.7549960127668));
#106983=CARTESIAN_POINT('',(96.5389396828847,10.7491495099393,14.2791510586097));
#106984=CARTESIAN_POINT('',(96.5386021580424,10.7493836819919,14.2078409669239));
#106985=CARTESIAN_POINT('',(96.5365,10.75,11.7549960127668));
#106986=CARTESIAN_POINT('Ctrl Pts',(96.5389396828847,10.7491495099393,14.2791510586097));
#106987=CARTESIAN_POINT('Ctrl Pts',(96.5397654834611,11.0277392116347,14.264058527972));
#106988=CARTESIAN_POINT('Ctrl Pts',(96.6161315948558,11.3070074359605,14.2489659973343));
#106989=CARTESIAN_POINT('Ctrl Pts',(96.7649096360069,11.5399149644685,14.2338734666966));
#106990=CARTESIAN_POINT('Ctrl Pts',(97.0238762976017,11.9453194492387,14.2076030423516));
#106991=CARTESIAN_POINT('Ctrl Pts',(97.5022346449331,12.2102615648714,14.1813326180065));
#106992=CARTESIAN_POINT('Ctrl Pts',(97.9833029979984,12.2156857424005,14.1550621936615));
#106993=CARTESIAN_POINT('Ctrl Pts',(98.4643713510638,12.2211099199297,14.1287917693165));
#106994=CARTESIAN_POINT('Ctrl Pts',(98.948149709863,11.9670161593553,14.1025213449715));
#106995=CARTESIAN_POINT('Ctrl Pts',(99.2164694661934,11.56786814773,14.0762509206264));
#106996=CARTESIAN_POINT('Ctrl Pts',(99.4847892225238,11.1687201361046,14.0499804962814));
#106997=CARTESIAN_POINT('Ctrl Pts',(99.5376503763853,10.6245178734282,14.0237100719364));
#106998=CARTESIAN_POINT('Ctrl Pts',(99.3510239773211,10.1811772819105,13.9974396475913));
#106999=CARTESIAN_POINT('Ctrl Pts',(99.1643975782568,9.73783669039288,13.9711692232463));
#107000=CARTESIAN_POINT('Ctrl Pts',(98.7382836262668,9.39535777003392,13.9448987989013));
#107001=CARTESIAN_POINT('Ctrl Pts',(98.2652009675881,9.30834068501235,13.9186283745563));
#107002=CARTESIAN_POINT('Ctrl Pts',(97.7921183089095,9.22132359999078,13.8923579502112));
#107003=CARTESIAN_POINT('Ctrl Pts',(97.2720669435421,9.3897683503066,13.8660875258662));
#107004=CARTESIAN_POINT('Ctrl Pts',(96.9398749827355,9.737636556329,13.8398171015212));
#107005=CARTESIAN_POINT('Ctrl Pts',(96.6841657298197,10.0054128109353,13.8195950872173));
#107006=CARTESIAN_POINT('Ctrl Pts',(96.5397699137549,10.3795039000482,13.7993730729135));
#107007=CARTESIAN_POINT('Ctrl Pts',(96.5364271352644,10.7512852130388,13.7791510586097));
#107008=CARTESIAN_POINT('Ctrl Pts',(96.5364532332071,10.7512863178753,13.7078409669239));
#107009=CARTESIAN_POINT('Ctrl Pts',(96.5397811846501,10.3803848363914,13.7280143518949));
#107010=CARTESIAN_POINT('Ctrl Pts',(96.6834082335339,10.0071884960508,13.7481877368659));
#107011=CARTESIAN_POINT('Ctrl Pts',(96.9380160986013,9.73958572435502,13.7683611218369));
#107012=CARTESIAN_POINT('Ctrl Pts',(97.2695745686609,9.39110487305198,13.7946315461819));
#107013=CARTESIAN_POINT('Ctrl Pts',(97.7893351702339,9.22169041697355,13.8209019705269));
#107014=CARTESIAN_POINT('Ctrl Pts',(98.2625669313284,9.30784856791217,13.8471723948719));
#107015=CARTESIAN_POINT('Ctrl Pts',(98.7357986924228,9.39400671885079,13.873442819217));
#107016=CARTESIAN_POINT('Ctrl Pts',(99.1625016130387,9.73573747680645,13.899713243562));
#107017=CARTESIAN_POINT('Ctrl Pts',(99.3499600818927,10.1787180107837,13.925983667907));
#107018=CARTESIAN_POINT('Ctrl Pts',(99.5374185507468,10.6216985447609,13.9522540922521));
#107019=CARTESIAN_POINT('Ctrl Pts',(99.485632567839,11.1659288547597,13.9785245165971));
#107020=CARTESIAN_POINT('Ctrl Pts',(99.2180052725653,11.5656030593164,14.0047949409421));
#107021=CARTESIAN_POINT('Ctrl Pts',(98.9503779772916,11.9652772638732,14.0310653652871));
#107022=CARTESIAN_POINT('Ctrl Pts',(98.4669093696519,12.2203953629878,14.0573357896322));
#107023=CARTESIAN_POINT('Ctrl Pts',(97.9859125610385,12.2157814107928,14.0836062139772));
#107024=CARTESIAN_POINT('Ctrl Pts',(97.5049157524252,12.2111674585977,14.1098766383222));
#107025=CARTESIAN_POINT('Ctrl Pts',(97.0263907428381,11.946821455093,14.1361470626673));
#107026=CARTESIAN_POINT('Ctrl Pts',(96.7665130736172,11.5420450822417,14.1624174870123));
#107027=CARTESIAN_POINT('Ctrl Pts',(96.6167305915848,11.3087491242799,14.1775586469828));
#107028=CARTESIAN_POINT('Ctrl Pts',(96.5395801623541,11.0288038634533,14.1926998069534));
#107029=CARTESIAN_POINT('Ctrl Pts',(96.5386021580424,10.7493836819919,14.2078409669239));
#107030=CARTESIAN_POINT('Origin',(98.,10.75,8.19412889803065));
#107031=CARTESIAN_POINT('',(96.8221913621849,10.7510342737659,13.9441288980306));
#107032=CARTESIAN_POINT('',(96.8239417093505,10.7495040187672,14.042863127503));
#107033=CARTESIAN_POINT('',(96.82225,10.7499999999999,8.19412889803065));
#107034=CARTESIAN_POINT('',(97.0688835974449,11.4739959996586,14.3914960127668));
#107035=CARTESIAN_POINT('Ctrl Pts',(96.8221913621849,10.7510342737659,13.9441288980306));
#107036=CARTESIAN_POINT('Ctrl Pts',(96.8248814594635,10.4518436749448,13.9643509123345));
#107037=CARTESIAN_POINT('Ctrl Pts',(97.092042366385,9.75970094281903,14.0108433509833));
#107038=CARTESIAN_POINT('Ctrl Pts',(98.2512181987561,9.38424363867761,14.0836062139772));
#107039=CARTESIAN_POINT('Ctrl Pts',(99.2799623879387,10.2110722313379,14.1624174870123));
#107040=CARTESIAN_POINT('Ctrl Pts',(99.1523425233119,11.5249107312363,14.2412287600474));
#107041=CARTESIAN_POINT('Ctrl Pts',(98.0207166727073,12.1192718941808,14.3175882686322));
#107042=CARTESIAN_POINT('Ctrl Pts',(97.2863392653372,11.7499101701945,14.367677352872));
#107043=CARTESIAN_POINT('Ctrl Pts',(97.0688835974449,11.4739959996586,14.3914960127668));
#107044=CARTESIAN_POINT('',(98.3831331782623,11.8636893777956,14.3914960127668));
#107045=CARTESIAN_POINT('Origin',(98.,10.75,14.3914960127668));
#107046=CARTESIAN_POINT('Ctrl Pts',(96.8239417093505,10.7495040187672,14.042863127503));
#107047=CARTESIAN_POINT('Ctrl Pts',(96.8233632025523,10.5842220536541,14.0539923918774));
#107048=CARTESIAN_POINT('Ctrl Pts',(96.9327137988548,10.0295622300994,14.091392080597));
#107049=CARTESIAN_POINT('Ctrl Pts',(97.7773396251973,9.37952591027267,14.1550621936615));
#107050=CARTESIAN_POINT('Ctrl Pts',(99.0247842083376,9.81167589004277,14.2338734666966));
#107051=CARTESIAN_POINT('Ctrl Pts',(99.3448716997135,11.0936334060014,14.3126847397317));
#107052=CARTESIAN_POINT('Ctrl Pts',(98.7507886462592,11.7372079631681,14.3652255884217));
#107053=CARTESIAN_POINT('Ctrl Pts',(98.3831331782623,11.8636893777956,14.3914960127668));
#107054=CARTESIAN_POINT('Origin',(98.,10.75,8.19412889803065));
#107055=CARTESIAN_POINT('',(96.8209354401503,10.7492853136663,13.4441288980306));
#107056=CARTESIAN_POINT('',(96.8222123644753,10.7510351628818,13.542863127503));
#107057=CARTESIAN_POINT('',(96.82225,10.7499999999999,8.19412889803065));
#107058=CARTESIAN_POINT('Ctrl Pts',(96.8209354401503,10.7492853136663,13.4441288980306));
#107059=CARTESIAN_POINT('Ctrl Pts',(96.8206175452072,10.7050856206175,13.4471246085859));
#107060=CARTESIAN_POINT('Ctrl Pts',(96.8428270438524,10.2736059300338,13.4763907434862));
#107061=CARTESIAN_POINT('Ctrl Pts',(97.3741854288762,9.51029866733518,13.5319273027316));
#107062=CARTESIAN_POINT('Ctrl Pts',(98.6934908176036,9.54684924260553,13.6107385757667));
#107063=CARTESIAN_POINT('Ctrl Pts',(99.3864080892004,10.670134243859,13.6895498488018));
#107064=CARTESIAN_POINT('Ctrl Pts',(98.82706002641,11.8655606324956,13.7683611218369));
#107065=CARTESIAN_POINT('Ctrl Pts',(97.5206840659668,12.0533593482333,13.8471723948719));
#107066=CARTESIAN_POINT('Ctrl Pts',(96.8713488287459,11.3178003010048,13.9057616536032));
#107067=CARTESIAN_POINT('Ctrl Pts',(96.8213867533488,10.8405222641786,13.9380804879894));
#107068=CARTESIAN_POINT('Ctrl Pts',(96.8221913621849,10.7510342737659,13.9441288980306));
#107069=CARTESIAN_POINT('Ctrl Pts',(96.8222123644753,10.7510351628818,13.542863127503));
#107070=CARTESIAN_POINT('Ctrl Pts',(96.824890529704,10.4525526074888,13.5630365124739));
#107071=CARTESIAN_POINT('Ctrl Pts',(97.0909910233665,9.7611248355653,13.60948032179));
#107072=CARTESIAN_POINT('Ctrl Pts',(98.2487444791565,9.38375846460147,13.682194555451));
#107073=CARTESIAN_POINT('Ctrl Pts',(99.2789105838822,10.2087808086717,13.7610058284861));
#107074=CARTESIAN_POINT('Ctrl Pts',(99.1538864471491,11.5226870217249,13.8398171015212));
#107075=CARTESIAN_POINT('Ctrl Pts',(97.986673971616,12.1386050426998,13.9186283745563));
#107076=CARTESIAN_POINT('Ctrl Pts',(96.9945380412469,11.5905309339865,13.9863103832169));
#107077=CARTESIAN_POINT('Ctrl Pts',(96.8247287572344,10.9743670995436,14.0277219675324));
#107078=CARTESIAN_POINT('Ctrl Pts',(96.8239417093505,10.7495040187672,14.042863127503));
#107079=CARTESIAN_POINT('Origin',(98.,10.75,8.19412889803065));
#107080=CARTESIAN_POINT('',(96.8240376082166,10.7497435860393,12.9441288980306));
#107081=CARTESIAN_POINT('',(96.8209186535446,10.749294419553,13.042863127503));
#107082=CARTESIAN_POINT('',(96.82225,10.7499999999999,8.19412889803065));
#107083=CARTESIAN_POINT('Ctrl Pts',(96.8240376082166,10.7497435860393,12.9441288980306));
#107084=CARTESIAN_POINT('Ctrl Pts',(96.8236844331119,10.570903593424,12.9561687291824));
#107085=CARTESIAN_POINT('Ctrl Pts',(96.9456229031997,10.0022988352385,12.9944789846792));
#107086=CARTESIAN_POINT('Ctrl Pts',(97.8247504499228,9.37239678178178,13.0590596645211));
#107087=CARTESIAN_POINT('Ctrl Pts',(99.0558897301026,9.8480022865368,13.1378709375562));
#107088=CARTESIAN_POINT('Ctrl Pts',(99.3333052969297,11.1383298048701,13.2166822105913));
#107089=CARTESIAN_POINT('Ctrl Pts',(98.4064237370152,12.0779016595067,13.2954934836263));
#107090=CARTESIAN_POINT('Ctrl Pts',(97.161629113368,11.8279341345178,13.3713090461061));
#107091=CARTESIAN_POINT('Ctrl Pts',(96.8234052761637,11.0926880511199,13.4208541842409));
#107092=CARTESIAN_POINT('Ctrl Pts',(96.8209354401503,10.7492853136663,13.4441288980306));
#107093=CARTESIAN_POINT('Ctrl Pts',(96.8209186535446,10.749294419553,13.042863127503));
#107094=CARTESIAN_POINT('Ctrl Pts',(96.8206089963791,10.7058138361133,13.0458102087254));
#107095=CARTESIAN_POINT('Ctrl Pts',(96.8424195706642,10.2750588747293,13.0750277142929));
#107096=CARTESIAN_POINT('Ctrl Pts',(97.3719134809519,9.51144811833339,13.1305156442054));
#107097=CARTESIAN_POINT('Ctrl Pts',(98.6912844455304,9.54557939774368,13.2093269172405));
#107098=CARTESIAN_POINT('Ctrl Pts',(99.3862585807745,10.6675934793599,13.2881381902756));
#107099=CARTESIAN_POINT('Ctrl Pts',(98.8291056640969,11.8640410388261,13.3669494633107));
#107100=CARTESIAN_POINT('Ctrl Pts',(97.5230705811704,12.0542392266786,13.4457607363457));
#107101=CARTESIAN_POINT('Ctrl Pts',(96.87185607722,11.3192549760816,13.5043986244099));
#107102=CARTESIAN_POINT('Ctrl Pts',(96.8214029376552,10.8412460965111,13.5367660881289));
#107103=CARTESIAN_POINT('Ctrl Pts',(96.8222123644753,10.7510351628818,13.542863127503));
#107104=CARTESIAN_POINT('Origin',(98.,10.75,8.19412889803065));
#107105=CARTESIAN_POINT('',(96.8218137388258,10.7509979852509,12.4441288980306));
#107106=CARTESIAN_POINT('',(96.8240326431611,10.7497324482223,12.542863127503));
#107107=CARTESIAN_POINT('',(96.82225,10.7499999999999,8.19412889803065));
#107108=CARTESIAN_POINT('Ctrl Pts',(96.8218137388257,10.7509979852509,12.4441288980306));
#107109=CARTESIAN_POINT('Ctrl Pts',(96.8246086178889,10.4393146543342,12.4652128497789));
#107110=CARTESIAN_POINT('Ctrl Pts',(97.1108125884919,9.7347364811699,12.5125672258722));
#107111=CARTESIAN_POINT('Ctrl Pts',(98.2954919596144,9.39309634609896,12.5861920263106));
#107112=CARTESIAN_POINT('Ctrl Pts',(99.2967249538166,10.2530015917544,12.6650032993457));
#107113=CARTESIAN_POINT('Ctrl Pts',(99.1267017686563,11.561816573295,12.7438145723807));
#107114=CARTESIAN_POINT('Ctrl Pts',(97.9389944505958,12.1373648936305,12.8226258454158));
#107115=CARTESIAN_POINT('Ctrl Pts',(96.9794154936065,11.5632993510555,12.8893972872991));
#107116=CARTESIAN_POINT('Ctrl Pts',(96.8244550468982,10.9611252200095,12.9298983048374));
#107117=CARTESIAN_POINT('Ctrl Pts',(96.8240376082166,10.7497435860393,12.9441288980306));
#107118=CARTESIAN_POINT('Ctrl Pts',(96.8240326431611,10.7497324482223,12.542863127503));
#107119=CARTESIAN_POINT('Ctrl Pts',(96.823665528048,10.5716166193381,12.5548543293219));
#107120=CARTESIAN_POINT('Ctrl Pts',(96.9449149417848,10.0037574602552,12.5931159554859));
#107121=CARTESIAN_POINT('Ctrl Pts',(97.8222251896378,9.37272024999355,12.6576480059949));
#107122=CARTESIAN_POINT('Ctrl Pts',(99.0542344468179,9.84606796723849,12.73645927903));
#107123=CARTESIAN_POINT('Ctrl Pts',(99.3340150885336,11.1358848763664,12.8152705520651));
#107124=CARTESIAN_POINT('Ctrl Pts',(98.4088575369805,12.0771544423753,12.8940818251001));
#107125=CARTESIAN_POINT('Ctrl Pts',(97.1628078249773,11.8293105708282,12.9699460169128));
#107126=CARTESIAN_POINT('Ctrl Pts',(96.8233692953073,11.0934018567722,13.0195397843804));
#107127=CARTESIAN_POINT('Ctrl Pts',(96.8209186535446,10.749294419553,13.042863127503));
#107128=CARTESIAN_POINT('Origin',(98.,10.75,8.19412889803065));
#107129=CARTESIAN_POINT('',(96.821256416619,10.7491427536305,11.9441288980306));
#107130=CARTESIAN_POINT('',(96.8218348096404,10.751001207122,12.042863127503));
#107131=CARTESIAN_POINT('',(96.82225,10.7499999999999,8.19412889803065));
#107132=CARTESIAN_POINT('Ctrl Pts',(96.821256416619,10.7491427536305,11.9441288980306));
#107133=CARTESIAN_POINT('Ctrl Pts',(96.820788807215,10.6921851792609,11.9479865460304));
#107134=CARTESIAN_POINT('Ctrl Pts',(96.850287974486,10.2478350064117,11.9781146183752));
#107135=CARTESIAN_POINT('Ctrl Pts',(97.4147916508613,9.49062149767907,12.034513115065));
#107136=CARTESIAN_POINT('Ctrl Pts',(98.7322138678675,9.57001445953124,12.1133243881001));
#107137=CARTESIAN_POINT('Ctrl Pts',(99.3882699138082,10.7152196834265,12.1921356611351));
#107138=CARTESIAN_POINT('Ctrl Pts',(98.7903825456925,11.8918399430189,12.2709469341702));
#107139=CARTESIAN_POINT('Ctrl Pts',(97.478588625315,12.0371026386346,12.3497582072053));
#107140=CARTESIAN_POINT('Ctrl Pts',(96.8626988373633,11.2919537648761,12.4074855284921));
#107141=CARTESIAN_POINT('Ctrl Pts',(96.8211262223751,10.8276694306214,12.4389424254339));
#107142=CARTESIAN_POINT('Ctrl Pts',(96.8218137388257,10.7509979852509,12.4441288980306));
#107143=CARTESIAN_POINT('Ctrl Pts',(96.8218348096404,10.751001207122,12.042863127503));
#107144=CARTESIAN_POINT('Ctrl Pts',(96.8246265753037,10.440022309364,12.0638984499184));
#107145=CARTESIAN_POINT('Ctrl Pts',(97.1097348020618,9.73614113337312,12.1112041966789));
#107146=CARTESIAN_POINT('Ctrl Pts',(98.2930039044064,9.39255677692249,12.1847803677844));
#107147=CARTESIAN_POINT('Ctrl Pts',(99.2958117603423,10.2506251171967,12.2635916408195));
#107148=CARTESIAN_POINT('Ctrl Pts',(99.1281882710963,11.5597497248036,12.3424029138546));
#107149=CARTESIAN_POINT('Ctrl Pts',(97.941537978492,12.1374745345601,12.4212141868896));
#107150=CARTESIAN_POINT('Ctrl Pts',(96.9802084953429,11.5647522740104,12.4880342581058));
#107151=CARTESIAN_POINT('Ctrl Pts',(96.824469806881,10.9618342537341,12.5285839049769));
#107152=CARTESIAN_POINT('Ctrl Pts',(96.8240326431611,10.7497324482223,12.542863127503));
#107153=CARTESIAN_POINT('Origin',(98.,10.75,8.19412889803065));
#107154=CARTESIAN_POINT('',(96.824088859708,10.7499448247057,11.4441288980306));
#107155=CARTESIAN_POINT('',(96.8212371046644,10.7491497734663,11.542863127503));
#107156=CARTESIAN_POINT('',(96.82225,10.7499999999999,8.19412889803065));
#107157=CARTESIAN_POINT('Ctrl Pts',(96.824088859708,10.7499448247057,11.4441288980306));
#107158=CARTESIAN_POINT('Ctrl Pts',(96.824007628141,10.5582806949243,11.4570306666269));
#107159=CARTESIAN_POINT('Ctrl Pts',(96.9584708630627,9.97645980746022,11.4962028595682));
#107160=CARTESIAN_POINT('Ctrl Pts',(97.8695993014189,9.36743040615582,11.5616454768545));
#107161=CARTESIAN_POINT('Ctrl Pts',(99.0846369462246,9.88278277294862,11.6404567498895));
#107162=CARTESIAN_POINT('Ctrl Pts',(99.3199851647595,11.1814419877856,11.7192680229246));
#107163=CARTESIAN_POINT('Ctrl Pts',(98.3630676087894,12.0904047655311,11.7980792959597));
#107164=CARTESIAN_POINT('Ctrl Pts',(97.1411032137602,11.8034278121455,11.8730329209951));
#107165=CARTESIAN_POINT('Ctrl Pts',(96.8239732080398,11.0800639199987,11.9217161216854));
#107166=CARTESIAN_POINT('Ctrl Pts',(96.821256416619,10.7491427536305,11.9441288980306));
#107167=CARTESIAN_POINT('Ctrl Pts',(96.8212371046644,10.7491497734663,11.542863127503));
#107168=CARTESIAN_POINT('Ctrl Pts',(96.8207779930583,10.6929125877714,11.5466721461699));
#107169=CARTESIAN_POINT('Ctrl Pts',(96.8498547297939,10.2492897535191,11.5767515891818));
#107170=CARTESIAN_POINT('Ctrl Pts',(97.412483782776,9.49169634572781,11.6331014565388));
#107171=CARTESIAN_POINT('Ctrl Pts',(98.7300494612188,9.56867397555541,11.7119127295739));
#107172=CARTESIAN_POINT('Ctrl Pts',(99.388203951153,10.7126746485813,11.790724002609));
#107173=CARTESIAN_POINT('Ctrl Pts',(98.7924746072532,11.89038913916,11.869535275644));
#107174=CARTESIAN_POINT('Ctrl Pts',(97.4809490736544,12.0380564924405,11.9483465486791));
#107175=CARTESIAN_POINT('Ctrl Pts',(96.8631742202878,11.2934111401974,12.0061224992988));
#107176=CARTESIAN_POINT('Ctrl Pts',(96.8211400174464,10.8283951350857,12.0376280255734));
#107177=CARTESIAN_POINT('Ctrl Pts',(96.8218348096404,10.751001207122,12.042863127503));
#107178=CARTESIAN_POINT('Origin',(98.,10.75,8.19412889803065));
#107179=CARTESIAN_POINT('',(96.821445951145,10.7509180827198,10.9441288980306));
#107180=CARTESIAN_POINT('',(96.8240876217551,10.7499333449883,11.042863127503));
#107181=CARTESIAN_POINT('',(96.82225,10.7499999999999,8.19412889803065));
#107182=CARTESIAN_POINT('Ctrl Pts',(96.821445951145,10.7509180827198,10.9441288980306));
#107183=CARTESIAN_POINT('Ctrl Pts',(96.8242284462551,10.4267547825223,10.9660747872234));
#107184=CARTESIAN_POINT('Ctrl Pts',(97.1302745778463,9.70993094798344,11.0142911007611));
#107185=CARTESIAN_POINT('Ctrl Pts',(98.3394198147195,9.4034127530893,11.0887778386439));
#107186=CARTESIAN_POINT('Ctrl Pts',(99.3121871841641,10.2953926774361,11.167589111679));
#107187=CARTESIAN_POINT('Ctrl Pts',(99.0997322410784,11.5979929374135,11.2464003847141));
#107188=CARTESIAN_POINT('Ctrl Pts',(97.8939531704686,12.1346505313534,11.3252116577492));
#107189=CARTESIAN_POINT('Ctrl Pts',(96.9656710215615,11.5375217036545,11.391121162188));
#107190=CARTESIAN_POINT('Ctrl Pts',(96.8241730308702,10.9485448655703,11.4307602422819));
#107191=CARTESIAN_POINT('Ctrl Pts',(96.824088859708,10.7499448247057,11.4441288980306));
#107192=CARTESIAN_POINT('Ctrl Pts',(96.8240876217551,10.7499333449883,11.042863127503));
#107193=CARTESIAN_POINT('Ctrl Pts',(96.8239898537243,10.5589920743739,11.0557162667664));
#107194=CARTESIAN_POINT('Ctrl Pts',(96.9577306106451,9.97791664978809,11.0948398303748));
#107195=CARTESIAN_POINT('Ctrl Pts',(97.8670648684311,9.36767165887723,11.1602338183283));
#107196=CARTESIAN_POINT('Ctrl Pts',(99.0830453734138,9.88079570239144,11.2390450913633));
#107197=CARTESIAN_POINT('Ctrl Pts',(99.3207740272075,11.1790213991231,11.3178563643984));
#107198=CARTESIAN_POINT('Ctrl Pts',(98.3655243729628,12.0897370356262,11.3966676374335));
#107199=CARTESIAN_POINT('Ctrl Pts',(97.1422426640937,11.8048160075092,11.4716698918017));
#107200=CARTESIAN_POINT('Ctrl Pts',(96.8239444403164,11.0807748854833,11.5204017218248));
#107201=CARTESIAN_POINT('Ctrl Pts',(96.8212371046644,10.7491497734663,11.542863127503));
#107202=CARTESIAN_POINT('Origin',(98.,10.75,8.19412889803065));
#107203=CARTESIAN_POINT('',(96.8216123189423,10.7490399772936,10.4441288980306));
#107204=CARTESIAN_POINT('',(96.8214660588487,10.7509237230245,10.542863127503));
#107205=CARTESIAN_POINT('',(96.82225,10.7499999999999,8.19412889803065));
#107206=CARTESIAN_POINT('Ctrl Pts',(96.8216123189423,10.7490399772936,10.4441288980306));
#107207=CARTESIAN_POINT('Ctrl Pts',(96.8209981027453,10.679301326976,10.4488484834748));
#107208=CARTESIAN_POINT('Ctrl Pts',(96.858210790406,10.2220336847976,10.4798384932641));
#107209=CARTESIAN_POINT('Ctrl Pts',(97.45601597308,9.47227374775156,10.5370989273983));
#107210=CARTESIAN_POINT('Ctrl Pts',(98.7701633646951,9.59442593343006,10.6159102004334));
#107211=CARTESIAN_POINT('Ctrl Pts',(99.3886670196609,10.7603409336293,10.6947214734685));
#107212=CARTESIAN_POINT('Ctrl Pts',(98.7528685749049,11.9169155624013,10.7735327465036));
#107213=CARTESIAN_POINT('Ctrl Pts',(97.4370477658578,12.0194832835491,10.8523440195387));
#107214=CARTESIAN_POINT('Ctrl Pts',(96.8545215587298,11.266137244336,10.909209403381));
#107215=CARTESIAN_POINT('Ctrl Pts',(96.8208976480979,10.8147959039589,10.9398043628784));
#107216=CARTESIAN_POINT('Ctrl Pts',(96.821445951145,10.7509180827198,10.9441288980306));
#107217=CARTESIAN_POINT('Ctrl Pts',(96.8214660588487,10.7509237230245,10.542863127503));
#107218=CARTESIAN_POINT('Ctrl Pts',(96.824252879472,10.4274642836231,10.5647603873629));
#107219=CARTESIAN_POINT('Ctrl Pts',(97.1291582504351,9.71132548914857,10.6129280715678));
#107220=CARTESIAN_POINT('Ctrl Pts',(98.3369506025399,9.40279263495737,10.6873661801177));
#107221=CARTESIAN_POINT('Ctrl Pts',(99.311351681027,10.2929877893503,10.7661774531528));
#107222=CARTESIAN_POINT('Ctrl Pts',(99.1012851078598,11.595975474055,10.8449887261879));
#107223=CARTESIAN_POINT('Ctrl Pts',(97.8964917932208,12.1348427503298,10.923799999223));
#107224=CARTESIAN_POINT('Ctrl Pts',(96.9664306987752,11.5389773547356,10.9897581329947));
#107225=CARTESIAN_POINT('Ctrl Pts',(96.8241896809885,10.9492553478996,11.0294458424213));
#107226=CARTESIAN_POINT('Ctrl Pts',(96.8240876217551,10.7499333449883,11.042863127503));
#107227=CARTESIAN_POINT('Origin',(98.,10.75,8.19412889803065));
#107228=CARTESIAN_POINT('',(96.8240738005051,10.7501486858619,9.94412889803064));
#107229=CARTESIAN_POINT('',(96.8215914858097,10.7490446521211,10.042863127503));
#107230=CARTESIAN_POINT('',(96.82225,10.7499999999999,8.19412889803065));
#107231=CARTESIAN_POINT('Ctrl Pts',(96.8240738005051,10.7501486858619,9.94412889803064));
#107232=CARTESIAN_POINT('Ctrl Pts',(96.8243065104756,10.5456862831697,9.95789260407134));
#107233=CARTESIAN_POINT('Ctrl Pts',(96.9718968717623,9.95065676196432,9.99792673445707));
#107234=CARTESIAN_POINT('Ctrl Pts',(97.9145860709853,9.36392434555335,10.0642312891878));
#107235=CARTESIAN_POINT('Ctrl Pts',(99.1122388935191,9.91847855386342,10.1430425622229));
#107236=CARTESIAN_POINT('Ctrl Pts',(99.3052714847173,11.2240987990573,10.221853835258));
#107237=CARTESIAN_POINT('Ctrl Pts',(98.319328101206,12.101492644125,10.3006651082931));
#107238=CARTESIAN_POINT('Ctrl Pts',(97.1212697594882,11.778722341383,10.374756795884));
#107239=CARTESIAN_POINT('Ctrl Pts',(96.8244169877987,11.0674845601755,10.4225780591298));
#107240=CARTESIAN_POINT('Ctrl Pts',(96.8216123189423,10.7490399772936,10.4441288980306));
#107241=CARTESIAN_POINT('Ctrl Pts',(96.8215914858097,10.7490446521211,10.042863127503));
#107242=CARTESIAN_POINT('Ctrl Pts',(96.8209852129159,10.6800276963346,10.0475340836143));
#107243=CARTESIAN_POINT('Ctrl Pts',(96.857751171539,10.2234899964845,10.0784754640707));
#107244=CARTESIAN_POINT('Ctrl Pts',(97.4536744407203,9.47327310866837,10.1356872688721));
#107245=CARTESIAN_POINT('Ctrl Pts',(98.7680436324125,9.59301580922626,10.2144985419072));
#107246=CARTESIAN_POINT('Ctrl Pts',(99.388683785519,10.7577951137743,10.2933098149423));
#107247=CARTESIAN_POINT('Ctrl Pts',(98.7550066620784,11.9155334853073,10.3721210879774));
#107248=CARTESIAN_POINT('Ctrl Pts',(97.4393759810305,12.0205133249269,10.4509323610125));
#107249=CARTESIAN_POINT('Ctrl Pts',(96.8549702624813,11.2675930892139,10.5078463741877));
#107250=CARTESIAN_POINT('Ctrl Pts',(96.8209094949199,10.8155227341254,10.5384899630178));
#107251=CARTESIAN_POINT('Ctrl Pts',(96.8214660588487,10.7509237230245,10.542863127503));
#107252=CARTESIAN_POINT('Origin',(98.,10.75,8.19412889803065));
#107253=CARTESIAN_POINT('',(96.8211250403637,10.7508514088176,9.44412889803064));
#107254=CARTESIAN_POINT('',(96.8240786690275,10.7501410021477,9.54286312750296));
#107255=CARTESIAN_POINT('',(96.82225,10.7499999999999,8.19412889803065));
#107256=CARTESIAN_POINT('Ctrl Pts',(96.8211250403636,10.7508514088176,9.44412889803065));
#107257=CARTESIAN_POINT('Ctrl Pts',(96.8237544514565,10.4142228729031,9.46693672466784));
#107258=CARTESIAN_POINT('Ctrl Pts',(97.1503930402075,9.68523305769091,9.51601497565005));
#107259=CARTESIAN_POINT('Ctrl Pts',(98.383005853651,9.41519382008176,9.59136365097731));
#107260=CARTESIAN_POINT('Ctrl Pts',(99.3262558620476,10.3382425252825,9.6701749240124));
#107261=CARTESIAN_POINT('Ctrl Pts',(99.0716056636518,11.6332844720055,9.74898619704748));
#107262=CARTESIAN_POINT('Ctrl Pts',(97.8490218626003,12.130469107685,9.82779747008258));
#107263=CARTESIAN_POINT('Ctrl Pts',(96.9525116359327,11.5117026075794,9.89284503707695));
#107264=CARTESIAN_POINT('Ctrl Pts',(96.8238623430648,10.9359383028979,9.93162217972631));
#107265=CARTESIAN_POINT('Ctrl Pts',(96.8240738005051,10.7501486858619,9.94412889803064));
#107266=CARTESIAN_POINT('Ctrl Pts',(96.8240786690275,10.7501410021477,9.54286312750296));
#107267=CARTESIAN_POINT('Ctrl Pts',(96.8242915248503,10.5463980025343,9.55657820421082));
#107268=CARTESIAN_POINT('Ctrl Pts',(96.9711196599306,9.95210488068972,9.59656370526371));
#107269=CARTESIAN_POINT('Ctrl Pts',(97.9120477433836,9.36408725039594,9.66281963066163));
#107270=CARTESIAN_POINT('Ctrl Pts',(99.1107114318979,9.91643879095944,9.74163090369672));
#107271=CARTESIAN_POINT('Ctrl Pts',(99.3061392069621,11.2217061208911,9.8204421767318));
#107272=CARTESIAN_POINT('Ctrl Pts',(98.321804948717,12.10090458802,9.89925344976689));
#107273=CARTESIAN_POINT('Ctrl Pts',(97.1223704965245,11.7801214664973,9.97339376669061));
#107274=CARTESIAN_POINT('Ctrl Pts',(96.8243950172063,11.0681933464253,10.0212636592693));
#107275=CARTESIAN_POINT('Ctrl Pts',(96.8215914858097,10.7490446521211,10.042863127503));
#107276=CARTESIAN_POINT('Origin',(98.,10.75,14.3914960127668));
#107277=CARTESIAN_POINT('',(97.7682422725578,9.30496691879707,14.3914960127668));
#107278=CARTESIAN_POINT('Ctrl Pts',(97.0688835974449,11.4739959996586,14.3914960127668));
#107279=CARTESIAN_POINT('Ctrl Pts',(97.0429761988506,11.4480386702715,14.3914960127668));
#107280=CARTESIAN_POINT('Ctrl Pts',(97.0184141797121,11.420872235244,14.3914960127668));
#107281=CARTESIAN_POINT('Ctrl Pts',(96.995310961042,11.3925593864603,14.3914960127668));
#107282=CARTESIAN_POINT('Ctrl Pts',(96.9647247406936,11.35507616631,14.3914960127668));
#107283=CARTESIAN_POINT('Ctrl Pts',(96.9366933909,11.3155851478366,14.3914960127668));
#107284=CARTESIAN_POINT('Ctrl Pts',(96.9112006310938,11.2743888078016,14.3914960127668));
#107285=CARTESIAN_POINT('Ctrl Pts',(96.9032600996146,11.2615568964134,14.3914960127668));
#107286=CARTESIAN_POINT('Ctrl Pts',(96.8955661051928,11.2485592386644,14.3914960127668));
#107287=CARTESIAN_POINT('Ctrl Pts',(96.8881188327785,11.2354042386312,14.3914960127668));
#107288=CARTESIAN_POINT('Ctrl Pts',(96.8811800017753,11.2231473589306,14.3914960127668));
#107289=CARTESIAN_POINT('Ctrl Pts',(96.8744542741059,11.2107513797533,14.3914960127668));
#107290=CARTESIAN_POINT('Ctrl Pts',(96.8679528845086,11.1982449409067,14.3914960127668));
#107291=CARTESIAN_POINT('Ctrl Pts',(96.8446356339814,11.1533905657889,14.3914960127668));
#107292=CARTESIAN_POINT('Ctrl Pts',(96.8241681434784,11.1070628521453,14.3914960127668));
#107293=CARTESIAN_POINT('Ctrl Pts',(96.8065305355175,11.0595945690794,14.3914960127668));
#107294=CARTESIAN_POINT('Ctrl Pts',(96.7939104221224,11.0256299228364,14.3914960127668));
#107295=CARTESIAN_POINT('Ctrl Pts',(96.7827398306571,10.991080304713,14.3914960127668));
#107296=CARTESIAN_POINT('Ctrl Pts',(96.7730236186375,10.9560568345071,14.3914960127668));
#107297=CARTESIAN_POINT('Ctrl Pts',(96.7696110617776,10.9437557872194,14.3914960127668));
#107298=CARTESIAN_POINT('Ctrl Pts',(96.766378010274,10.931396221671,14.3914960127668));
#107299=CARTESIAN_POINT('Ctrl Pts',(96.7633249962767,10.9189827643307,14.3914960127668));
#107300=CARTESIAN_POINT('Ctrl Pts',(96.7610658690711,10.9097972253134,14.3914960127668));
#107301=CARTESIAN_POINT('Ctrl Pts',(96.7589059318967,10.900584374175,14.3914960127668));
#107302=CARTESIAN_POINT('Ctrl Pts',(96.7568470780902,10.8913548727577,14.3914960127668));
#107303=CARTESIAN_POINT('Ctrl Pts',(96.7454259124535,10.8401556743983,14.3914960127668));
#107304=CARTESIAN_POINT('Ctrl Pts',(96.7370933376322,10.7883715386039,14.3914960127668));
#107305=CARTESIAN_POINT('Ctrl Pts',(96.7318320440446,10.736340937265,14.3914960127668));
#107306=CARTESIAN_POINT('Ctrl Pts',(96.7264686405729,10.6833005388905,14.3914960127668));
#107307=CARTESIAN_POINT('Ctrl Pts',(96.7242964061771,10.6300029496301,14.3914960127668));
#107308=CARTESIAN_POINT('Ctrl Pts',(96.7253427957507,10.5767796518361,14.3914960127668));
#107309=CARTESIAN_POINT('Ctrl Pts',(96.7259617653546,10.5452965365773,14.3914960127668));
#107310=CARTESIAN_POINT('Ctrl Pts',(96.7277078521842,10.5138389806834,14.3914960127668));
#107311=CARTESIAN_POINT('Ctrl Pts',(96.7305951134011,10.482473675579,14.3914960127668));
#107312=CARTESIAN_POINT('Ctrl Pts',(96.7320811103492,10.4663307830031,14.3914960127668));
#107313=CARTESIAN_POINT('Ctrl Pts',(96.7338694964227,10.4502123161242,14.3914960127668));
#107314=CARTESIAN_POINT('Ctrl Pts',(96.7359628745836,10.4341273667755,14.3914960127668));
#107315=CARTESIAN_POINT('Ctrl Pts',(96.7374537227486,10.4226720943033,14.3914960127668));
#107316=CARTESIAN_POINT('Ctrl Pts',(96.7390997168083,10.4112319328867,14.3914960127668));
#107317=CARTESIAN_POINT('Ctrl Pts',(96.7408980733302,10.3998319062154,14.3914960127668));
#107318=CARTESIAN_POINT('Ctrl Pts',(96.7494385785201,10.3456924818211,14.3914960127668));
#107319=CARTESIAN_POINT('Ctrl Pts',(96.7614239701143,10.2923517591577,14.3914960127668));
#107320=CARTESIAN_POINT('Ctrl Pts',(96.7768661020469,10.2401573800707,14.3914960127668));
#107321=CARTESIAN_POINT('Ctrl Pts',(96.7802201578377,10.2288206773286,14.3914960127668));
#107322=CARTESIAN_POINT('Ctrl Pts',(96.7837374792372,10.2175380043515,14.3914960127668));
#107323=CARTESIAN_POINT('Ctrl Pts',(96.7874185073135,10.2063128612481,14.3914960127668));
#107324=CARTESIAN_POINT('Ctrl Pts',(96.8037952935392,10.1563725279636,14.3914960127668));
#107325=CARTESIAN_POINT('Ctrl Pts',(96.8234081998674,10.1075702746358,14.3914960127668));
#107326=CARTESIAN_POINT('Ctrl Pts',(96.8460023865325,10.0600579930232,14.3914960127668));
#107327=CARTESIAN_POINT('Ctrl Pts',(96.8569215707814,10.0370965399424,14.3914960127668));
#107328=CARTESIAN_POINT('Ctrl Pts',(96.8685378258048,10.0144364777629,14.3914960127668));
#107329=CARTESIAN_POINT('Ctrl Pts',(96.8808264862297,9.99209596216232,14.3914960127668));
#107330=CARTESIAN_POINT('Ctrl Pts',(96.8886074358317,9.97795036614436,14.3914960127668));
#107331=CARTESIAN_POINT('Ctrl Pts',(96.8966580166366,9.96393289812474,14.3914960127668));
#107332=CARTESIAN_POINT('Ctrl Pts',(96.9049724672611,9.95004837447309,14.3914960127668));
#107333=CARTESIAN_POINT('Ctrl Pts',(96.910186650653,9.94134107005839,14.3914960127668));
#107334=CARTESIAN_POINT('Ctrl Pts',(96.9155049177142,9.93268578036605,14.3914960127668));
#107335=CARTESIAN_POINT('Ctrl Pts',(96.9209173591067,9.92409670769064,14.3914960127668));
#107336=CARTESIAN_POINT('Ctrl Pts',(96.9501434809259,9.87771740006923,14.3914960127668));
#107337=CARTESIAN_POINT('Ctrl Pts',(96.9821663853327,9.83317419115088,14.3914960127668));
#107338=CARTESIAN_POINT('Ctrl Pts',(97.0166886585068,9.79062429455657,14.3914960127668));
#107339=CARTESIAN_POINT('Ctrl Pts',(97.0519654053717,9.74714448302404,14.3914960127668));
#107340=CARTESIAN_POINT('Ctrl Pts',(97.0898524425345,9.70574520992445,14.3914960127668));
#107341=CARTESIAN_POINT('Ctrl Pts',(97.130085198549,9.66660954170395,14.3914960127668));
#107342=CARTESIAN_POINT('Ctrl Pts',(97.1526979511723,9.64461340542393,14.3914960127668));
#107343=CARTESIAN_POINT('Ctrl Pts',(97.1760526165578,9.62333268371835,14.3914960127668));
#107344=CARTESIAN_POINT('Ctrl Pts',(97.2001083672487,9.60280352273155,14.3914960127668));
#107345=CARTESIAN_POINT('Ctrl Pts',(97.2158596822888,9.58936136138041,14.3914960127668));
#107346=CARTESIAN_POINT('Ctrl Pts',(97.2319116681868,9.57624148376674,14.3914960127668));
#107347=CARTESIAN_POINT('Ctrl Pts',(97.2482537342435,9.56345483580649,14.3914960127668));
#107348=CARTESIAN_POINT('Ctrl Pts',(97.2564933326357,9.5570078637034,14.3914960127668));
#107349=CARTESIAN_POINT('Ctrl Pts',(97.2648087003651,9.55064411016295,14.3914960127668));
#107350=CARTESIAN_POINT('Ctrl Pts',(97.2731919630714,9.54436995193093,14.3914960127668));
#107351=CARTESIAN_POINT('Ctrl Pts',(97.3197937996518,9.50949244577978,14.3914960127668));
#107352=CARTESIAN_POINT('Ctrl Pts',(97.3683447994762,9.47748800785936,14.3914960127668));
#107353=CARTESIAN_POINT('Ctrl Pts',(97.4185523047113,9.44853887199522,14.3914960127668));
#107354=CARTESIAN_POINT('Ctrl Pts',(97.4688918883076,9.41951358109408,14.3914960127668));
#107355=CARTESIAN_POINT('Ctrl Pts',(97.5208974737716,9.39355880028942,14.3914960127668));
#107356=CARTESIAN_POINT('Ctrl Pts',(97.5743161192772,9.37088902478583,14.3914960127668));
#107357=CARTESIAN_POINT('Ctrl Pts',(97.6265065651117,9.34874047198558,14.3914960127668));
#107358=CARTESIAN_POINT('Ctrl Pts',(97.6800466921163,9.32972692287584,14.3914960127668));
#107359=CARTESIAN_POINT('Ctrl Pts',(97.7347284624306,9.31408912061954,14.3914960127668));
#107360=CARTESIAN_POINT('Ctrl Pts',(97.7458529634341,9.3109077542173,14.3914960127668));
#107361=CARTESIAN_POINT('Ctrl Pts',(97.7570247849795,9.30786626056828,14.3914960127668));
#107362=CARTESIAN_POINT('Ctrl Pts',(97.7682422725578,9.30496691879707,14.3914960127668));
#107363=CARTESIAN_POINT('',(96.5365,10.75,14.3914960127668));
#107364=CARTESIAN_POINT('Origin',(98.,10.75,14.3914960127668));
#107365=CARTESIAN_POINT('',(98.9846501585944,9.66583019221064,14.3914960127668));
#107366=CARTESIAN_POINT('Origin',(98.,10.75,14.3914960127668));
#107367=CARTESIAN_POINT('Ctrl Pts',(98.985638815547,9.6652849966315,14.3914960127668));
#107368=CARTESIAN_POINT('Ctrl Pts',(99.016139412943,9.69833171151842,14.3914960127668));
#107369=CARTESIAN_POINT('Ctrl Pts',(99.0449589200137,9.73279368715152,14.3914960127668));
#107370=CARTESIAN_POINT('Ctrl Pts',(99.0719485462807,9.76863256666571,14.3914960127668));
#107371=CARTESIAN_POINT('Ctrl Pts',(99.1063284484702,9.81428481690756,14.3914960127668));
#107372=CARTESIAN_POINT('Ctrl Pts',(99.1377406776653,9.8621714511127,14.3914960127668));
#107373=CARTESIAN_POINT('Ctrl Pts',(99.1661298440887,9.91196072331448,14.3914960127668));
#107374=CARTESIAN_POINT('Ctrl Pts',(99.1769248568896,9.93089315066194,14.3914960127668));
#107375=CARTESIAN_POINT('Ctrl Pts',(99.1872822730401,9.95010081750062,14.3914960127668));
#107376=CARTESIAN_POINT('Ctrl Pts',(99.1971972321457,9.9695657815029,14.3914960127668));
#107377=CARTESIAN_POINT('Ctrl Pts',(99.2030514614112,9.98105875496862,14.3914960127668));
#107378=CARTESIAN_POINT('Ctrl Pts',(99.2087516966422,9.99264230536428,14.3914960127668));
#107379=CARTESIAN_POINT('Ctrl Pts',(99.2142900149449,10.0042976336629,14.3914960127668));
#107380=CARTESIAN_POINT('Ctrl Pts',(99.238975512711,10.0562479848257,14.3914960127668));
#107381=CARTESIAN_POINT('Ctrl Pts',(99.260484301343,10.1096920623883,14.3914960127668));
#107382=CARTESIAN_POINT('Ctrl Pts',(99.2787659465126,10.1642873542009,14.3914960127668));
#107383=CARTESIAN_POINT('Ctrl Pts',(99.2910846217951,10.2010751632604,14.3914960127668));
#107384=CARTESIAN_POINT('Ctrl Pts',(99.3019369735001,10.2383860468379,14.3914960127668));
#107385=CARTESIAN_POINT('Ctrl Pts',(99.3112942427666,10.2761157654541,14.3914960127668));
#107386=CARTESIAN_POINT('Ctrl Pts',(99.3153448835169,10.2924484722911,14.3914960127668));
#107387=CARTESIAN_POINT('Ctrl Pts',(99.3191152218517,10.3088596507996,14.3914960127668));
#107388=CARTESIAN_POINT('Ctrl Pts',(99.3226022941674,10.3253407262825,14.3914960127668));
#107389=CARTESIAN_POINT('Ctrl Pts',(99.3249788512658,10.3365731336955,14.3914960127668));
#107390=CARTESIAN_POINT('Ctrl Pts',(99.327224111217,10.3478400238607,14.3914960127668));
#107391=CARTESIAN_POINT('Ctrl Pts',(99.3293340464886,10.3591211859305,14.3914960127668));
#107392=CARTESIAN_POINT('Ctrl Pts',(99.339673988808,10.4144056141612,14.3914960127668));
#107393=CARTESIAN_POINT('Ctrl Pts',(99.3467877541545,10.4701190818833,14.3914960127668));
#107394=CARTESIAN_POINT('Ctrl Pts',(99.3506248509382,10.5259436282514,14.3914960127668));
#107395=CARTESIAN_POINT('Ctrl Pts',(99.3543694449217,10.5804223845209,14.3914960127668));
#107396=CARTESIAN_POINT('Ctrl Pts',(99.3549932689645,10.6350079682248,14.3914960127668));
#107397=CARTESIAN_POINT('Ctrl Pts',(99.3524014399336,10.6893967205018,14.3914960127668));
#107398=CARTESIAN_POINT('Ctrl Pts',(99.3508330094634,10.7223097619436,14.3914960127668));
#107399=CARTESIAN_POINT('Ctrl Pts',(99.3480860911869,10.7551504957268,14.3914960127668));
#107400=CARTESIAN_POINT('Ctrl Pts',(99.3441311915637,10.7878477780733,14.3914960127668));
#107401=CARTESIAN_POINT('Ctrl Pts',(99.3411589614533,10.8124208030236,14.3914960127668));
#107402=CARTESIAN_POINT('Ctrl Pts',(99.3375043339722,10.8369127499246,14.3914960127668));
#107403=CARTESIAN_POINT('Ctrl Pts',(99.3331524064438,10.8612918325753,14.3914960127668));
#107404=CARTESIAN_POINT('Ctrl Pts',(99.331461276709,10.8707653799422,14.3914960127668));
#107405=CARTESIAN_POINT('Ctrl Pts',(99.3296656034321,10.8802171964784,14.3914960127668));
#107406=CARTESIAN_POINT('Ctrl Pts',(99.3277664602594,10.8896377701555,14.3914960127668));
#107407=CARTESIAN_POINT('Ctrl Pts',(99.3173475530846,10.9413200677745,14.3914960127668));
#107408=CARTESIAN_POINT('Ctrl Pts',(99.3038056233175,10.9921354570883,14.3914960127668));
#107409=CARTESIAN_POINT('Ctrl Pts',(99.2870604116319,11.0418039394557,14.3914960127668));
#107410=CARTESIAN_POINT('Ctrl Pts',(99.2833577555898,11.0527865003091,14.3914960127668));
#107411=CARTESIAN_POINT('Ctrl Pts',(99.2794982983791,11.0637129030486,14.3914960127668));
#107412=CARTESIAN_POINT('Ctrl Pts',(99.2754808601922,11.074579962025,14.3914960127668));
#107413=CARTESIAN_POINT('Ctrl Pts',(99.2565155778308,11.1258805253043,14.3914960127668));
#107414=CARTESIAN_POINT('Ctrl Pts',(99.2340328831329,11.1758617007157,14.3914960127668));
#107415=CARTESIAN_POINT('Ctrl Pts',(99.2082809266655,11.2242819327261,14.3914960127668));
#107416=CARTESIAN_POINT('Ctrl Pts',(99.1972654713244,11.2449937921917,14.3914960127668));
#107417=CARTESIAN_POINT('Ctrl Pts',(99.1856513303607,11.2654195472256,14.3914960127668));
#107418=CARTESIAN_POINT('Ctrl Pts',(99.1734560041558,11.285537825985,14.3914960127668));
#107419=CARTESIAN_POINT('Ctrl Pts',(99.1644844946234,11.3003378671345,14.3914960127668));
#107420=CARTESIAN_POINT('Ctrl Pts',(99.1551984345818,11.3149714760779,14.3914960127668));
#107421=CARTESIAN_POINT('Ctrl Pts',(99.1456045021247,11.3294295540173,14.3914960127668));
#107422=CARTESIAN_POINT('Ctrl Pts',(99.140099525536,11.337725566203,14.3914960127668));
#107423=CARTESIAN_POINT('Ctrl Pts',(99.1344983585284,11.3459559325157,14.3914960127668));
#107424=CARTESIAN_POINT('Ctrl Pts',(99.1288044719674,11.3541169102581,14.3914960127668));
#107425=CARTESIAN_POINT('Ctrl Pts',(99.0987571404528,11.3971833818293,14.3914960127668));
#107426=CARTESIAN_POINT('Ctrl Pts',(99.066115553153,11.4383434819937,14.3914960127668));
#107427=CARTESIAN_POINT('Ctrl Pts',(99.0311189048726,11.4773986149495,14.3914960127668));
#107428=CARTESIAN_POINT('Ctrl Pts',(98.996294801149,11.5162611937342,14.3914960127668));
#107429=CARTESIAN_POINT('Ctrl Pts',(98.9591377847492,11.5530401413719,14.3914960127668));
#107430=CARTESIAN_POINT('Ctrl Pts',(98.9198553772279,11.5874972110253,14.3914960127668));
#107431=CARTESIAN_POINT('Ctrl Pts',(98.9002209306982,11.6047198186599,14.3914960127668));
#107432=CARTESIAN_POINT('Ctrl Pts',(98.8800551562504,11.6213616305313,14.3914960127668));
#107433=CARTESIAN_POINT('Ctrl Pts',(98.859382499797,11.6373881384408,14.3914960127668));
#107434=CARTESIAN_POINT('Ctrl Pts',(98.8441369891611,11.6492072434185,14.3914960127668));
#107435=CARTESIAN_POINT('Ctrl Pts',(98.8286157834736,11.6606916398438,14.3914960127668));
#107436=CARTESIAN_POINT('Ctrl Pts',(98.8128285365262,11.6718262543508,14.3914960127668));
#107437=CARTESIAN_POINT('Ctrl Pts',(98.8051889947957,11.6772143598555,14.3914960127668));
#107438=CARTESIAN_POINT('Ctrl Pts',(98.7974879290995,11.6825198806233,14.3914960127668));
#107439=CARTESIAN_POINT('Ctrl Pts',(98.7897372384311,11.6877341666513,14.3914960127668));
#107440=CARTESIAN_POINT('Ctrl Pts',(98.7478945384241,11.715883891025,14.3914960127668));
#107441=CARTESIAN_POINT('Ctrl Pts',(98.7045253466422,11.7414367511671,14.3914960127668));
#107442=CARTESIAN_POINT('Ctrl Pts',(98.6598266413956,11.7641882725167,14.3914960127668));
#107443=CARTESIAN_POINT('Ctrl Pts',(98.6160321815113,11.7864795353968,14.3914960127668));
#107444=CARTESIAN_POINT('Ctrl Pts',(98.57096057418,11.8060819970254,14.3914960127668));
#107445=CARTESIAN_POINT('Ctrl Pts',(98.5247867566208,11.8227547930337,14.3914960127668));
#107446=CARTESIAN_POINT('Ctrl Pts',(98.4786129390616,11.8394275890421,14.3914960127668));
#107447=CARTESIAN_POINT('Ctrl Pts',(98.431336115872,11.8531711940639,14.3914960127668));
#107448=CARTESIAN_POINT('Ctrl Pts',(98.3831331782623,11.8636893777956,14.3914960127668));
#107449=CARTESIAN_POINT('Ctrl Pts',(97.4897834946116,11.8114961988294,8.95351817334586));
#107450=CARTESIAN_POINT('Ctrl Pts',(97.1393582418089,11.6430615420855,8.97978859769089));
#107451=CARTESIAN_POINT('Ctrl Pts',(96.6242618069232,10.9346841371649,9.03232944638095));
#107452=CARTESIAN_POINT('Ctrl Pts',(97.0914565134647,9.69872289948882,9.11114071941605));
#107453=CARTESIAN_POINT('Ctrl Pts',(98.3807382620766,9.41477895129228,9.18995199245111));
#107454=CARTESIAN_POINT('Ctrl Pts',(99.3254100117742,10.3356711404167,9.2687632654862));
#107455=CARTESIAN_POINT('Ctrl Pts',(99.0732671457231,11.6313879250538,9.3475745385213));
#107456=CARTESIAN_POINT('Ctrl Pts',(97.8515312358663,12.1307094457997,9.42638581155637));
#107457=CARTESIAN_POINT('Ctrl Pts',(96.7639840600833,11.3830590515328,9.50519708459147));
#107458=CARTESIAN_POINT('Ctrl Pts',(96.7928159215348,10.0635328883854,9.58400835762655));
#107459=CARTESIAN_POINT('Ctrl Pts',(97.9120477433836,9.36408725039594,9.66281963066163));
#107460=CARTESIAN_POINT('Ctrl Pts',(99.1107114318979,9.91643879095944,9.74163090369672));
#107461=CARTESIAN_POINT('Ctrl Pts',(99.3061392069621,11.2217061208911,9.8204421767318));
#107462=CARTESIAN_POINT('Ctrl Pts',(98.321804948717,12.10090458802,9.89925344976689));
#107463=CARTESIAN_POINT('Ctrl Pts',(97.0468042470516,11.7599116273157,9.97806472280198));
#107464=CARTESIAN_POINT('Ctrl Pts',(96.632769181073,10.5067232539037,10.0568759958371));
#107465=CARTESIAN_POINT('Ctrl Pts',(97.4536744407203,9.47327310866837,10.1356872688721));
#107466=CARTESIAN_POINT('Ctrl Pts',(98.7680436324125,9.59301580922626,10.2144985419072));
#107467=CARTESIAN_POINT('Ctrl Pts',(99.388683785519,10.7577951137743,10.2933098149423));
#107468=CARTESIAN_POINT('Ctrl Pts',(98.7550066620784,11.9155334853073,10.3721210879774));
#107469=CARTESIAN_POINT('Ctrl Pts',(97.4393759810305,12.0205133249269,10.4509323610125));
#107470=CARTESIAN_POINT('Ctrl Pts',(96.6301243384503,10.977912408914,10.5297436340476));
#107471=CARTESIAN_POINT('Ctrl Pts',(97.0582016567961,9.7294514859898,10.6085549070827));
#107472=CARTESIAN_POINT('Ctrl Pts',(98.3369506025399,9.40279263495737,10.6873661801177));
#107473=CARTESIAN_POINT('Ctrl Pts',(99.311351681027,10.2929877893503,10.7661774531528));
#107474=CARTESIAN_POINT('Ctrl Pts',(99.1012851078598,11.595975474055,10.8449887261879));
#107475=CARTESIAN_POINT('Ctrl Pts',(97.8964917932208,12.1348427503298,10.923799999223));
#107476=CARTESIAN_POINT('Ctrl Pts',(96.7851914173279,11.4228621696346,11.0026112722581));
#107477=CARTESIAN_POINT('Ctrl Pts',(96.7711569308156,10.1031243526508,11.0814225452932));
#107478=CARTESIAN_POINT('Ctrl Pts',(97.8670648684311,9.36767165887723,11.1602338183283));
#107479=CARTESIAN_POINT('Ctrl Pts',(99.0830453734138,9.88079570239144,11.2390450913633));
#107480=CARTESIAN_POINT('Ctrl Pts',(99.3207740272075,11.1790213991231,11.3178563643984));
#107481=CARTESIAN_POINT('Ctrl Pts',(98.3655243729628,12.0897370356262,11.3966676374335));
#107482=CARTESIAN_POINT('Ctrl Pts',(97.0801178266041,11.7903461822508,11.4754789104686));
#107483=CARTESIAN_POINT('Ctrl Pts',(96.625587309158,10.5512711719255,11.5542901835037));
#107484=CARTESIAN_POINT('Ctrl Pts',(97.412483782776,9.49169634572781,11.6331014565388));
#107485=CARTESIAN_POINT('Ctrl Pts',(98.7300494612188,9.56867397555541,11.7119127295739));
#107486=CARTESIAN_POINT('Ctrl Pts',(99.388203951153,10.7126746485813,11.790724002609));
#107487=CARTESIAN_POINT('Ctrl Pts',(98.7924746072532,11.89038913916,11.869535275644));
#107488=CARTESIAN_POINT('Ctrl Pts',(97.4809490736544,12.0380564924405,11.9483465486791));
#107489=CARTESIAN_POINT('Ctrl Pts',(96.6382520323991,11.0222973826287,12.0271578217142));
#107490=CARTESIAN_POINT('Ctrl Pts',(97.0255426748034,9.76058789514945,12.1059690947493));
#107491=CARTESIAN_POINT('Ctrl Pts',(98.2930039044064,9.39255677692249,12.1847803677844));
#107492=CARTESIAN_POINT('Ctrl Pts',(99.2958117603423,10.2506251171967,12.2635916408195));
#107493=CARTESIAN_POINT('Ctrl Pts',(99.1281882710963,11.5597497248036,12.3424029138546));
#107494=CARTESIAN_POINT('Ctrl Pts',(97.941537978492,12.1374745345601,12.4212141868896));
#107495=CARTESIAN_POINT('Ctrl Pts',(96.807693027503,11.4619743498409,12.5000254599247));
#107496=CARTESIAN_POINT('Ctrl Pts',(96.7507895706755,10.1433891731248,12.5788367329598));
#107497=CARTESIAN_POINT('Ctrl Pts',(97.8222251896378,9.37272024999355,12.6576480059949));
#107498=CARTESIAN_POINT('Ctrl Pts',(99.0542344468179,9.84606796723849,12.73645927903));
#107499=CARTESIAN_POINT('Ctrl Pts',(99.3340150885336,11.1358848763664,12.8152705520651));
#107500=CARTESIAN_POINT('Ctrl Pts',(98.4088575369805,12.0771544423753,12.8940818251001));
#107501=CARTESIAN_POINT('Ctrl Pts',(97.1144027787922,11.8196826290748,12.9728930981352));
#107502=CARTESIAN_POINT('Ctrl Pts',(96.6198564263835,10.5960287813665,13.0517043711703));
#107503=CARTESIAN_POINT('Ctrl Pts',(97.3719134809519,9.51144811833339,13.1305156442054));
#107504=CARTESIAN_POINT('Ctrl Pts',(98.6912844455304,9.54557939774368,13.2093269172405));
#107505=CARTESIAN_POINT('Ctrl Pts',(99.3862585807745,10.6675934793599,13.2881381902756));
#107506=CARTESIAN_POINT('Ctrl Pts',(98.8291056640969,11.8640410388261,13.3669494633107));
#107507=CARTESIAN_POINT('Ctrl Pts',(97.5230705811704,12.0542392266786,13.4457607363457));
#107508=CARTESIAN_POINT('Ctrl Pts',(96.6478166153533,11.0663959334999,13.5245720093808));
#107509=CARTESIAN_POINT('Ctrl Pts',(96.9939141781605,9.79276675085979,13.6033832824159));
#107510=CARTESIAN_POINT('Ctrl Pts',(98.2487444791565,9.38375846460147,13.682194555451));
#107511=CARTESIAN_POINT('Ctrl Pts',(99.2789105838822,10.2087808086717,13.7610058284861));
#107512=CARTESIAN_POINT('Ctrl Pts',(99.1538864471491,11.5226870217249,13.8398171015212));
#107513=CARTESIAN_POINT('Ctrl Pts',(97.986673971616,12.1386050426998,13.9186283745563));
#107514=CARTESIAN_POINT('Ctrl Pts',(96.8313965612137,11.5004085842898,13.9974396475913));
#107515=CARTESIAN_POINT('Ctrl Pts',(96.731856377117,10.1841450230525,14.0762509206264));
#107516=CARTESIAN_POINT('Ctrl Pts',(97.7773396251973,9.37952591027267,14.1550621936615));
#107517=CARTESIAN_POINT('Ctrl Pts',(99.0247842083376,9.81167589004277,14.2338734666966));
#107518=CARTESIAN_POINT('Ctrl Pts',(99.3448716997135,11.0936334060014,14.3126847397317));
#107519=CARTESIAN_POINT('Ctrl Pts',(98.7507886462592,11.7372079631681,14.3652255884217));
#107520=CARTESIAN_POINT('Ctrl Pts',(98.3831331782623,11.8636893777956,14.3914960127668));
#107521=CARTESIAN_POINT('Ctrl Pts',(97.4485199648826,11.8973442250985,9.00851078648618));
#107522=CARTESIAN_POINT('Ctrl Pts',(97.0697542278266,11.7152874914666,9.03478121083121));
#107523=CARTESIAN_POINT('Ctrl Pts',(96.5129996011151,10.9496203834523,9.08732205952127));
#107524=CARTESIAN_POINT('Ctrl Pts',(97.0179784688096,9.6137013381866,9.16613333255634));
#107525=CARTESIAN_POINT('Ctrl Pts',(98.4115302972817,9.30679355125881,9.24494460559144));
#107526=CARTESIAN_POINT('Ctrl Pts',(99.4326019486213,10.30216248079,9.32375587862652));
#107527=CARTESIAN_POINT('Ctrl Pts',(99.1600671420125,11.7026697759231,9.40256715166161));
#107528=CARTESIAN_POINT('Ctrl Pts',(97.8395238915373,12.2423736994294,9.48137842469669));
#107529=CARTESIAN_POINT('Ctrl Pts',(96.6640218284744,11.4342574167704,9.56018969773178));
#107530=CARTESIAN_POINT('Ctrl Pts',(96.695185453716,10.0080151703796,9.63900097076685));
#107531=CARTESIAN_POINT('Ctrl Pts',(97.9049346443025,9.2520021819181,9.71781224380195));
#107532=CARTESIAN_POINT('Ctrl Pts',(99.2005397179419,9.84902490417435,9.79662351683703));
#107533=CARTESIAN_POINT('Ctrl Pts',(99.4117726261623,11.2598551406448,9.87543478987212));
#107534=CARTESIAN_POINT('Ctrl Pts',(98.3478307787874,12.210158387221,9.9542460629072));
#107535=CARTESIAN_POINT('Ctrl Pts',(96.9697149704917,11.841587774632,10.0330573359423));
#107536=CARTESIAN_POINT('Ctrl Pts',(96.5221950053118,10.4870483567985,10.1118686089774));
#107537=CARTESIAN_POINT('Ctrl Pts',(97.4094906075456,9.37001839722762,10.1906798820125));
#107538=CARTESIAN_POINT('Ctrl Pts',(98.8301588147409,9.49944523468055,10.2694911550476));
#107539=CARTESIAN_POINT('Ctrl Pts',(99.5009929602766,10.7584255400846,10.3483024280826));
#107540=CARTESIAN_POINT('Ctrl Pts',(98.8160674853117,12.0097954801921,10.4271137011177));
#107541=CARTESIAN_POINT('Ctrl Pts',(97.3940357663781,12.1232655169875,10.5059249741528));
#107542=CARTESIAN_POINT('Ctrl Pts',(96.5193362622349,10.99634472218,10.5847362471879));
#107543=CARTESIAN_POINT('Ctrl Pts',(96.9820341406084,9.64691508526005,10.663547520223));
#107544=CARTESIAN_POINT('Ctrl Pts',(98.3642013305314,9.293837846997,10.742358793258));
#107545=CARTESIAN_POINT('Ctrl Pts',(99.417406656716,10.2560271329594,10.8211700662932));
#107546=CARTESIAN_POINT('Ctrl Pts',(99.1903510441992,11.6643933589234,10.8999813393282));
#107547=CARTESIAN_POINT('Ctrl Pts',(97.8881206136871,12.2468412830989,10.9787926123633));
#107548=CARTESIAN_POINT('Ctrl Pts',(96.6869443211705,11.4772795940945,11.0576038853984));
#107549=CARTESIAN_POINT('Ctrl Pts',(96.6717748018918,10.0508085764589,11.1364151584335));
#107550=CARTESIAN_POINT('Ctrl Pts',(97.8563137996289,9.25587647781848,11.2152264314686));
#107551=CARTESIAN_POINT('Ctrl Pts',(99.1706361794572,9.81049919689602,11.2940377045037));
#107552=CARTESIAN_POINT('Ctrl Pts',(99.4275910308938,11.2137183112577,11.3728489775388));
#107553=CARTESIAN_POINT('Ctrl Pts',(98.3950859917484,12.1980876640647,11.4516602505738));
#107554=CARTESIAN_POINT('Ctrl Pts',(97.0057227707638,11.8744837104693,11.5304715236089));
#107555=CARTESIAN_POINT('Ctrl Pts',(96.5144323027452,10.535199067596,11.609282796644));
#107556=CARTESIAN_POINT('Ctrl Pts',(97.3649686737201,9.38993160527404,11.6880940696791));
#107557=CARTESIAN_POINT('Ctrl Pts',(98.78909188209,9.4731347661915,11.7669053427142));
#107558=CARTESIAN_POINT('Ctrl Pts',(99.5004743195226,10.7096559776218,11.8457166157493));
#107559=CARTESIAN_POINT('Ctrl Pts',(98.8565656336517,11.9826175963921,11.9245278887844));
#107560=CARTESIAN_POINT('Ctrl Pts',(97.4389710641154,12.1422274802604,12.0033391618194));
#107561=CARTESIAN_POINT('Ctrl Pts',(96.5281212797658,11.0443193106231,12.0821504348545));
#107562=CARTESIAN_POINT('Ctrl Pts',(96.9467338781784,9.68056963746572,12.1609617078896));
#107563=CARTESIAN_POINT('Ctrl Pts',(98.3167004630095,9.28277416856067,12.2397729809247));
#107564=CARTESIAN_POINT('Ctrl Pts',(99.4006099519555,10.210238398804,12.3185842539598));
#107565=CARTESIAN_POINT('Ctrl Pts',(99.2194299886273,11.6252378685416,12.3973955269949));
#107566=CARTESIAN_POINT('Ctrl Pts',(97.9368098888729,12.2496859116918,12.4762068000299));
#107567=CARTESIAN_POINT('Ctrl Pts',(96.7112657389187,11.5195549542326,12.555018073065));
#107568=CARTESIAN_POINT('Ctrl Pts',(96.6497602406877,10.0943297961264,12.6338293461001));
#107569=CARTESIAN_POINT('Ctrl Pts',(97.807847732039,9.26133337146405,12.7126406191352));
#107570=CARTESIAN_POINT('Ctrl Pts',(99.1394951821687,9.7729628718273,12.7914518921703));
#107571=CARTESIAN_POINT('Ctrl Pts',(99.4419029570818,11.1670931416807,12.8702631652054));
#107572=CARTESIAN_POINT('Ctrl Pts',(98.4419237058598,12.1844874592602,12.9490744382405));
#107573=CARTESIAN_POINT('Ctrl Pts',(97.0427805029951,11.9061927291974,13.0278857112756));
#107574=CARTESIAN_POINT('Ctrl Pts',(96.5082379374112,10.5835764285116,13.1066969843106));
#107575=CARTESIAN_POINT('Ctrl Pts',(97.3211172670363,9.41128079357963,13.1855082573457));
#107576=CARTESIAN_POINT('Ctrl Pts',(98.7471917632435,9.44817242481657,13.2643195303808));
#107577=CARTESIAN_POINT('Ctrl Pts',(99.4983716181923,10.6609288891744,13.3431308034159));
#107578=CARTESIAN_POINT('Ctrl Pts',(98.8961592106945,11.9541386053284,13.421942076451));
#107579=CARTESIAN_POINT('Ctrl Pts',(97.4844991295521,12.1597189858305,13.5007533494861));
#107580=CARTESIAN_POINT('Ctrl Pts',(96.538459394052,11.0919843119044,13.5795646225211));
#107581=CARTESIAN_POINT('Ctrl Pts',(96.9125474411364,9.71535094361666,13.6583758955562));
#107582=CARTESIAN_POINT('Ctrl Pts',(98.2688615767066,9.27326429669935,13.7371871685913));
#107583=CARTESIAN_POINT('Ctrl Pts',(99.3823419004731,10.1650099507019,13.8159984416264));
#107584=CARTESIAN_POINT('Ctrl Pts',(99.2472064930764,11.5851777360694,13.8948097146615));
#107585=CARTESIAN_POINT('Ctrl Pts',(97.9855962350814,12.2509078491674,13.9736209876966));
#107586=CARTESIAN_POINT('Ctrl Pts',(96.7368862852262,11.561097540056,14.0524322607317));
#107587=CARTESIAN_POINT('Ctrl Pts',(96.6292958336403,10.1383817570332,14.1312435337667));
#107588=CARTESIAN_POINT('Ctrl Pts',(97.759332067821,9.26868943644842,14.2100548068018));
#107589=CARTESIAN_POINT('Ctrl Pts',(99.1076631689353,9.73578935090167,14.2888660798369));
#107590=CARTESIAN_POINT('Ctrl Pts',(99.4536375917939,11.1214246027084,14.367677352872));
#107591=CARTESIAN_POINT('Ctrl Pts',(98.8115083393657,11.8170479618875,14.4202182015621));
#107592=CARTESIAN_POINT('Ctrl Pts',(98.4141189012336,11.9537585038707,14.4464886259071));
#107593=CARTESIAN_POINT('Ctrl Pts',(97.4072564351537,11.9831922513677,9.06350339962649));
#107594=CARTESIAN_POINT('Ctrl Pts',(97.0001502138443,11.7875134408477,9.08977382397152));
#107595=CARTESIAN_POINT('Ctrl Pts',(96.401737395307,10.9645566297397,9.14231467266158));
#107596=CARTESIAN_POINT('Ctrl Pts',(96.9445004241546,9.52867977688438,9.22112594569665));
#107597=CARTESIAN_POINT('Ctrl Pts',(98.4423223324868,9.19880815122535,9.29993721873175));
#107598=CARTESIAN_POINT('Ctrl Pts',(99.5397938854681,10.2686538211633,9.37874849176682));
#107599=CARTESIAN_POINT('Ctrl Pts',(99.2468671383022,11.7739516267925,9.45755976480192));
#107600=CARTESIAN_POINT('Ctrl Pts',(97.8275165472081,12.3540379530592,9.536371037837));
#107601=CARTESIAN_POINT('Ctrl Pts',(96.5640595968658,11.4854557820079,9.61518231087209));
#107602=CARTESIAN_POINT('Ctrl Pts',(96.597554985897,9.95249745237383,9.69399358390716));
#107603=CARTESIAN_POINT('Ctrl Pts',(97.8978215452215,9.13991711344024,9.77280485694227));
#107604=CARTESIAN_POINT('Ctrl Pts',(99.2903680039858,9.78161101738929,9.85161612997734));
#107605=CARTESIAN_POINT('Ctrl Pts',(99.5174060453627,11.2980041603985,9.93042740301244));
#107606=CARTESIAN_POINT('Ctrl Pts',(98.3738566088577,12.3194121864219,10.0092386760475));
#107607=CARTESIAN_POINT('Ctrl Pts',(96.8926256939319,11.9232639219484,10.0880499490826));
#107608=CARTESIAN_POINT('Ctrl Pts',(96.4116208295505,10.4673734596933,10.1668612221177));
#107609=CARTESIAN_POINT('Ctrl Pts',(97.3653067743711,9.26676368578688,10.2456724951528));
#107610=CARTESIAN_POINT('Ctrl Pts',(98.8922739970692,9.40587466013485,10.3244837681879));
#107611=CARTESIAN_POINT('Ctrl Pts',(99.6133021350342,10.7590559663949,10.4032950412229));
#107612=CARTESIAN_POINT('Ctrl Pts',(98.8771283085448,12.1040574750769,10.482106314258));
#107613=CARTESIAN_POINT('Ctrl Pts',(97.3486955517258,12.226017709048,10.5609175872931));
#107614=CARTESIAN_POINT('Ctrl Pts',(96.4085481860195,11.0147770354461,10.6397288603282));
#107615=CARTESIAN_POINT('Ctrl Pts',(96.9058666244206,9.5643786845303,10.7185401333633));
#107616=CARTESIAN_POINT('Ctrl Pts',(98.3914520585228,9.18488305903664,10.7973514063984));
#107617=CARTESIAN_POINT('Ctrl Pts',(99.5234616324051,10.2190664765685,10.8761626794335));
#107618=CARTESIAN_POINT('Ctrl Pts',(99.2794169805385,11.7328112437917,10.9549739524685));
#107619=CARTESIAN_POINT('Ctrl Pts',(97.8797494341536,12.3588398158681,11.0337852255036));
#107620=CARTESIAN_POINT('Ctrl Pts',(96.5886972250129,11.5316970185545,11.1125964985387));
#107621=CARTESIAN_POINT('Ctrl Pts',(96.5723926729683,9.99849280026701,11.1914077715738));
#107622=CARTESIAN_POINT('Ctrl Pts',(97.8455627308264,9.14408129675973,11.2702190446089));
#107623=CARTESIAN_POINT('Ctrl Pts',(99.2582269855007,9.74020269140061,11.349030317644));
#107624=CARTESIAN_POINT('Ctrl Pts',(99.5344080345801,11.2484152233922,11.4278415906791));
#107625=CARTESIAN_POINT('Ctrl Pts',(98.424647610534,12.3064382925031,11.5066528637141));
#107626=CARTESIAN_POINT('Ctrl Pts',(96.9313277149234,11.9586212386879,11.5854641367492));
#107627=CARTESIAN_POINT('Ctrl Pts',(96.4032772963324,10.5191269632665,11.6642754097843));
#107628=CARTESIAN_POINT('Ctrl Pts',(97.3174535646642,9.28816686482028,11.7430866828194));
#107629=CARTESIAN_POINT('Ctrl Pts',(98.8481343029613,9.37759555682758,11.8218979558545));
#107630=CARTESIAN_POINT('Ctrl Pts',(99.6127446878923,10.7066373066622,11.9007092288896));
#107631=CARTESIAN_POINT('Ctrl Pts',(98.9206566600503,12.074846053624,11.9795205019247));
#107632=CARTESIAN_POINT('Ctrl Pts',(97.3969930545765,12.2463984680804,12.0583317749597));
#107633=CARTESIAN_POINT('Ctrl Pts',(96.4179905271324,11.0663412386175,12.1371430479948));
#107634=CARTESIAN_POINT('Ctrl Pts',(96.8679250815535,9.60055137978199,12.2159543210299));
#107635=CARTESIAN_POINT('Ctrl Pts',(98.3403970216125,9.17299156019885,12.294765594065));
#107636=CARTESIAN_POINT('Ctrl Pts',(99.5054081435689,10.1698516804113,12.3735768671001));
#107637=CARTESIAN_POINT('Ctrl Pts',(99.3106717061581,11.6907260122797,12.4523881401352));
#107638=CARTESIAN_POINT('Ctrl Pts',(97.9320817992542,12.3618972888235,12.5311994131703));
#107639=CARTESIAN_POINT('Ctrl Pts',(96.6148384503341,11.5771355586244,12.6100106862053));
#107640=CARTESIAN_POINT('Ctrl Pts',(96.5487309106999,10.0452704191281,12.6888219592404));
#107641=CARTESIAN_POINT('Ctrl Pts',(97.7934702744402,9.14994649293456,12.7676332322755));
#107642=CARTESIAN_POINT('Ctrl Pts',(99.2247559175195,9.6998577764161,12.8464445053106));
#107643=CARTESIAN_POINT('Ctrl Pts',(99.5497908256302,11.1983014069949,12.9252557783457));
#107644=CARTESIAN_POINT('Ctrl Pts',(98.4749898747389,12.2918204761452,13.0040670513808));
#107645=CARTESIAN_POINT('Ctrl Pts',(96.9711582271979,11.99270282932,13.0828783244159));
#107646=CARTESIAN_POINT('Ctrl Pts',(96.3966194484392,10.5711240756567,13.1616895974509));
#107647=CARTESIAN_POINT('Ctrl Pts',(97.2703210531204,9.31111346882587,13.240500870486));
#107648=CARTESIAN_POINT('Ctrl Pts',(98.8030990809567,9.35076545188944,13.3193121435211));
#107649=CARTESIAN_POINT('Ctrl Pts',(99.6104846556101,10.6542642989889,13.3981234165562));
#107650=CARTESIAN_POINT('Ctrl Pts',(98.963212757292,12.0442361718308,13.4769346895913));
#107651=CARTESIAN_POINT('Ctrl Pts',(97.4459276779337,12.2651987449824,13.5557459626264));
#107652=CARTESIAN_POINT('Ctrl Pts',(96.4291021727508,11.1175726903089,13.6345572356614));
#107653=CARTESIAN_POINT('Ctrl Pts',(96.8311807041122,9.63793513637353,13.7133685086966));
#107654=CARTESIAN_POINT('Ctrl Pts',(98.2889786742568,9.16277012879724,13.7921797817316));
#107655=CARTESIAN_POINT('Ctrl Pts',(99.4857732170638,10.121239092732,13.8709910547667));
#107656=CARTESIAN_POINT('Ctrl Pts',(99.3405265390038,11.647668450414,13.9498023278018));
#107657=CARTESIAN_POINT('Ctrl Pts',(97.9845184985468,12.3632106556349,14.0286136008369));
#107658=CARTESIAN_POINT('Ctrl Pts',(96.6423760092385,11.6217864958221,14.107424873872));
#107659=CARTESIAN_POINT('Ctrl Pts',(96.5267352901637,10.0926184910139,14.1862361469071));
#107660=CARTESIAN_POINT('Ctrl Pts',(97.7413245104446,9.15785296262414,14.2650474199421));
#107661=CARTESIAN_POINT('Ctrl Pts',(99.1905421295333,9.65990281176058,14.3438586929772));
#107662=CARTESIAN_POINT('Ctrl Pts',(99.5624034838743,11.1492157994153,14.4226699660123));
#107663=CARTESIAN_POINT('Ctrl Pts',(98.8722280324722,11.8968879606069,14.4752108147024));
#107664=CARTESIAN_POINT('Ctrl Pts',(98.4451046242049,12.0438276299459,14.5014812390474));
#107665=CARTESIAN_POINT('Ctrl Pts',(97.3659929054248,12.0690402776369,9.1184960127668));
#107666=CARTESIAN_POINT('Ctrl Pts',(96.930546199862,11.8597393902289,9.14476643711183));
#107667=CARTESIAN_POINT('Ctrl Pts',(96.2904751894988,10.9794928760271,9.19730728580189));
#107668=CARTESIAN_POINT('Ctrl Pts',(96.8710223794995,9.44365821558217,9.27611855883696));
#107669=CARTESIAN_POINT('Ctrl Pts',(98.4731143676917,9.09082275119189,9.35492983187206));
#107670=CARTESIAN_POINT('Ctrl Pts',(99.6469858223152,10.2351451615366,9.43374110490715));
#107671=CARTESIAN_POINT('Ctrl Pts',(99.3336671345917,11.8452334776618,9.51255237794222));
#107672=CARTESIAN_POINT('Ctrl Pts',(97.815509202879,12.4657022066889,9.59136365097732));
#107673=CARTESIAN_POINT('Ctrl Pts',(96.464097365257,11.5366541472455,9.6701749240124));
#107674=CARTESIAN_POINT('Ctrl Pts',(96.4999245180781,9.89697973436806,9.74898619704748));
#107675=CARTESIAN_POINT('Ctrl Pts',(97.8907084461403,9.02783204496239,9.82779747008258));
#107676=CARTESIAN_POINT('Ctrl Pts',(99.3801962900298,9.71419713060421,9.90660874311765));
#107677=CARTESIAN_POINT('Ctrl Pts',(99.623039464563,11.3361531801521,9.98542001615274));
#107678=CARTESIAN_POINT('Ctrl Pts',(98.399882438928,12.4286659856228,10.0642312891878));
#107679=CARTESIAN_POINT('Ctrl Pts',(96.8155364173721,12.0049400692647,10.1430425622229));
#107680=CARTESIAN_POINT('Ctrl Pts',(96.3010466537892,10.447698562588,10.221853835258));
#107681=CARTESIAN_POINT('Ctrl Pts',(97.3211229411965,9.16350897434615,10.3006651082931));
#107682=CARTESIAN_POINT('Ctrl Pts',(98.9543891793977,9.31230408558914,10.3794763813282));
#107683=CARTESIAN_POINT('Ctrl Pts',(99.7256113097918,10.7596863927053,10.4582876543633));
#107684=CARTESIAN_POINT('Ctrl Pts',(98.9381891317781,12.1983194699616,10.5370989273983));
#107685=CARTESIAN_POINT('Ctrl Pts',(97.3033553370735,12.3287699011085,10.6159102004334));
#107686=CARTESIAN_POINT('Ctrl Pts',(96.2977601098042,11.0332093487121,10.6947214734685));
#107687=CARTESIAN_POINT('Ctrl Pts',(96.8296991082329,9.48184228380054,10.7735327465036));
#107688=CARTESIAN_POINT('Ctrl Pts',(98.4187027865141,9.07592827107629,10.8523440195387));
#107689=CARTESIAN_POINT('Ctrl Pts',(99.6295166080943,10.1821058201776,10.9311552925738));
#107690=CARTESIAN_POINT('Ctrl Pts',(99.3684829168778,11.8012291286601,11.0099665656089));
#107691=CARTESIAN_POINT('Ctrl Pts',(97.8713782546199,12.4708383486373,11.0887778386439));
#107692=CARTESIAN_POINT('Ctrl Pts',(96.4904501288555,11.5861144430144,11.167589111679));
#107693=CARTESIAN_POINT('Ctrl Pts',(96.4730105440447,9.94617702407511,11.2464003847141));
#107694=CARTESIAN_POINT('Ctrl Pts',(97.8348116620241,9.03228611570099,11.3252116577492));
#107695=CARTESIAN_POINT('Ctrl Pts',(99.3458177915441,9.66990618590519,11.4040229307843));
#107696=CARTESIAN_POINT('Ctrl Pts',(99.6412250382663,11.2831121355268,11.4828342038194));
#107697=CARTESIAN_POINT('Ctrl Pts',(98.4542092293196,12.4147889209416,11.5616454768544));
#107698=CARTESIAN_POINT('Ctrl Pts',(96.856932659083,12.0427587669064,11.6404567498895));
#107699=CARTESIAN_POINT('Ctrl Pts',(96.2921222899196,10.503054858937,11.7192680229246));
#107700=CARTESIAN_POINT('Ctrl Pts',(97.2699384556081,9.18640212436651,11.7980792959597));
#107701=CARTESIAN_POINT('Ctrl Pts',(98.9071767238326,9.28205634746367,11.8768905689948));
#107702=CARTESIAN_POINT('Ctrl Pts',(99.7250150562619,10.7036186357026,11.9557018420299));
#107703=CARTESIAN_POINT('Ctrl Pts',(98.9847476864488,12.1670745108561,12.034513115065));
#107704=CARTESIAN_POINT('Ctrl Pts',(97.3550150450377,12.3505694559004,12.1133243881001));
#107705=CARTESIAN_POINT('Ctrl Pts',(96.3078597744989,11.0883631666119,12.1921356611351));
#107706=CARTESIAN_POINT('Ctrl Pts',(96.7891162849286,9.52053312209826,12.2709469341702));
#107707=CARTESIAN_POINT('Ctrl Pts',(98.3640935802155,9.06320895183703,12.3497582072053));
#107708=CARTESIAN_POINT('Ctrl Pts',(99.6102063351822,10.1294649620185,12.4285694802404));
#107709=CARTESIAN_POINT('Ctrl Pts',(99.401913423689,11.7562141560178,12.5073807532755));
#107710=CARTESIAN_POINT('Ctrl Pts',(97.9273537096352,12.4741086659552,12.5861920263106));
#107711=CARTESIAN_POINT('Ctrl Pts',(96.5184111617498,11.6347161630161,12.6650032993457));
#107712=CARTESIAN_POINT('Ctrl Pts',(96.447701580712,9.99621104212966,12.7438145723807));
#107713=CARTESIAN_POINT('Ctrl Pts',(97.7790928168414,9.03855961440507,12.8226258454158));
#107714=CARTESIAN_POINT('Ctrl Pts',(99.3100166528703,9.62675268100489,12.9014371184509));
#107715=CARTESIAN_POINT('Ctrl Pts',(99.6576786941785,11.2295096723092,12.980248391486));
#107716=CARTESIAN_POINT('Ctrl Pts',(98.5080560436181,12.3991534930301,13.0590596645211));
#107717=CARTESIAN_POINT('Ctrl Pts',(96.8995359514008,12.0792129294426,13.1378709375562));
#107718=CARTESIAN_POINT('Ctrl Pts',(96.285000959467,10.5586717228019,13.2166822105912));
#107719=CARTESIAN_POINT('Ctrl Pts',(97.2195248392047,9.2109461440721,13.2954934836263));
#107720=CARTESIAN_POINT('Ctrl Pts',(98.85900639867,9.25335847896233,13.3743047566614));
#107721=CARTESIAN_POINT('Ctrl Pts',(99.7225976930278,10.6475997088034,13.4531160296965));
#107722=CARTESIAN_POINT('Ctrl Pts',(99.0302663038896,12.1343337383332,13.5319273027316));
#107723=CARTESIAN_POINT('Ctrl Pts',(97.4073562263153,12.3706785041343,13.6107385757667));
#107724=CARTESIAN_POINT('Ctrl Pts',(96.3197449514496,11.1431610687133,13.6895498488018));
#107725=CARTESIAN_POINT('Ctrl Pts',(96.7498139670879,9.56051932913041,13.7683611218369));
#107726=CARTESIAN_POINT('Ctrl Pts',(98.3090957718069,9.05227596089513,13.8471723948719));
#107727=CARTESIAN_POINT('Ctrl Pts',(99.5892045336545,10.0774682347621,13.925983667907));
#107728=CARTESIAN_POINT('Ctrl Pts',(99.4338465849312,11.7101591647585,14.0047949409421));
#107729=CARTESIAN_POINT('Ctrl Pts',(97.9834407620123,12.4755134621025,14.0836062139772));
#107730=CARTESIAN_POINT('Ctrl Pts',(96.547865733251,11.6824754515883,14.1624174870123));
#107731=CARTESIAN_POINT('Ctrl Pts',(96.4241747466871,10.0468552249946,14.2412287600474));
#107732=CARTESIAN_POINT('Ctrl Pts',(97.7233169530683,9.04701648879988,14.3200400330824));
#107733=CARTESIAN_POINT('Ctrl Pts',(99.2734210901312,9.58401627261947,14.3988513061175));
#107734=CARTESIAN_POINT('Ctrl Pts',(99.6711693759547,11.1770069961223,14.4776625791526));
#107735=CARTESIAN_POINT('Ctrl Pts',(98.9329477255787,11.9767279593263,14.5302034278427));
#107736=CARTESIAN_POINT('Ctrl Pts',(98.4760903471762,12.1338967560211,14.5564738521877));
#107737=CARTESIAN_POINT('Ctrl Pts',(96.5386021580424,10.7493836819919,14.2078409669239));
#107738=CARTESIAN_POINT('Ctrl Pts',(96.5378832918151,10.5440004037554,14.2189702312984));
#107739=CARTESIAN_POINT('Ctrl Pts',(96.5783184588143,10.3389008126099,14.2300994956729));
#107740=CARTESIAN_POINT('Ctrl Pts',(96.6613136121779,10.1528188067278,14.2412287600474));
#107741=CARTESIAN_POINT('Ctrl Pts',(96.8572221488142,9.71357564626303,14.2674991843924));
#107742=CARTESIAN_POINT('Ctrl Pts',(97.2902695509412,9.38029606753146,14.2937696087374));
#107743=CARTESIAN_POINT('Ctrl Pts',(97.7651439415152,9.30315624213561,14.3200400330824));
#107744=CARTESIAN_POINT('Ctrl Pts',(98.195699285931,9.23321571733423,14.3438586929772));
#107745=CARTESIAN_POINT('Ctrl Pts',(98.6606386832877,9.37383596121387,14.367677352872));
#107746=CARTESIAN_POINT('Ctrl Pts',(98.9856388155471,9.66528499663154,14.3914960127668));
#107747=CARTESIAN_POINT('',(97.3153355754606,9.7917048010816,9.1184960127668));
#107748=CARTESIAN_POINT('Ctrl Pts',(97.3138573448686,9.79064797878732,9.1184960127668));
#107749=CARTESIAN_POINT('Ctrl Pts',(97.2816262023953,9.80814453001893,9.1184960127668));
#107750=CARTESIAN_POINT('Ctrl Pts',(97.2503400185293,9.8271834909513,9.1184960127668));
#107751=CARTESIAN_POINT('Ctrl Pts',(97.2201253783783,9.84773709665585,9.1184960127668));
#107752=CARTESIAN_POINT('Ctrl Pts',(97.1801243676892,9.8749479122531,9.1184960127668));
#107753=CARTESIAN_POINT('Ctrl Pts',(97.1419999996926,9.90481142917744,9.1184960127668));
#107754=CARTESIAN_POINT('Ctrl Pts',(97.1058228801383,9.93703307814226,9.1184960127668));
#107755=CARTESIAN_POINT('Ctrl Pts',(97.0945544245732,9.947069483032,9.1184960127668));
#107756=CARTESIAN_POINT('Ctrl Pts',(97.0834750376363,9.95733502451731,9.1184960127668));
#107757=CARTESIAN_POINT('Ctrl Pts',(97.0725872918701,9.96782169999479,9.1184960127668));
#107758=CARTESIAN_POINT('Ctrl Pts',(97.0624427997589,9.97759250094279,9.1184960127668));
#107759=CARTESIAN_POINT('Ctrl Pts',(97.0524629268139,9.98755737105614,9.1184960127668));
#107760=CARTESIAN_POINT('Ctrl Pts',(97.0426666047809,9.99769206046759,9.1184960127668));
#107761=CARTESIAN_POINT('Ctrl Pts',(97.0075321550023,10.0340400628046,9.1184960127668));
#107762=CARTESIAN_POINT('Ctrl Pts',(96.9747093356107,10.0726125260596,9.1184960127668));
#107763=CARTESIAN_POINT('Ctrl Pts',(96.9442739384259,10.1130848201818,9.1184960127668));
#107764=CARTESIAN_POINT('Ctrl Pts',(96.9224967199919,10.1420436664974,9.1184960127668));
#107765=CARTESIAN_POINT('Ctrl Pts',(96.9019421721014,10.1719763617394,9.1184960127668));
#107766=CARTESIAN_POINT('Ctrl Pts',(96.8826466217712,10.2027777804103,9.1184960127668));
#107767=CARTESIAN_POINT('Ctrl Pts',(96.8758695774648,10.2135959522408,9.1184960127668));
#107768=CARTESIAN_POINT('Ctrl Pts',(96.869247914313,10.2245213776691,9.1184960127668));
#107769=CARTESIAN_POINT('Ctrl Pts',(96.8627834610163,10.2355497738227,9.1184960127668));
#107770=CARTESIAN_POINT('Ctrl Pts',(96.8579999807869,10.2437104198265,9.1184960127668));
#107771=CARTESIAN_POINT('Ctrl Pts',(96.8533037921159,10.2519255162684,9.1184960127668));
#107772=CARTESIAN_POINT('Ctrl Pts',(96.8486997486209,10.2601853832081,9.1184960127668));
#107773=CARTESIAN_POINT('Ctrl Pts',(96.8231595708657,10.3060056431825,9.1184960127668));
#107774=CARTESIAN_POINT('Ctrl Pts',(96.8004131575191,10.3532668875542,9.1184960127668));
#107775=CARTESIAN_POINT('Ctrl Pts',(96.7805403871832,10.4016397520554,9.1184960127668));
#107776=CARTESIAN_POINT('Ctrl Pts',(96.7602819368002,10.4509514111153,9.1184960127668));
#107777=CARTESIAN_POINT('Ctrl Pts',(96.743008985931,10.5014191405875,9.1184960127668));
#107778=CARTESIAN_POINT('Ctrl Pts',(96.7288423286544,10.5527330349271,9.1184960127668));
#107779=CARTESIAN_POINT('Ctrl Pts',(96.7204623441663,10.5830866765937,9.1184960127668));
#107780=CARTESIAN_POINT('Ctrl Pts',(96.7131700098127,10.6137370708059,9.1184960127668));
#107781=CARTESIAN_POINT('Ctrl Pts',(96.7069978078214,10.6446242994682,9.1184960127668));
#107782=CARTESIAN_POINT('Ctrl Pts',(96.7038211368344,10.6605211484857,9.1184960127668));
#107783=CARTESIAN_POINT('Ctrl Pts',(96.7009412741981,10.6764807723151,9.1184960127668));
#107784=CARTESIAN_POINT('Ctrl Pts',(96.6983633062362,10.6924951981886,9.1184960127668));
#107785=CARTESIAN_POINT('Ctrl Pts',(96.6965273501873,10.7039002204718,9.1184960127668));
#107786=CARTESIAN_POINT('Ctrl Pts',(96.6948444111156,10.7153349782316,9.1184960127668));
#107787=CARTESIAN_POINT('Ctrl Pts',(96.6933189532335,10.7267746925458,9.1184960127668));
#107788=CARTESIAN_POINT('Ctrl Pts',(96.6860744472355,10.7811026946108,9.1184960127668));
#107789=CARTESIAN_POINT('Ctrl Pts',(96.6823595818324,10.8356469910512,9.1184960127668));
#107790=CARTESIAN_POINT('Ctrl Pts',(96.6822848029741,10.8900777405499,9.1184960127668));
#107791=CARTESIAN_POINT('Ctrl Pts',(96.6822685608941,10.9019001808453,9.1184960127668));
#107792=CARTESIAN_POINT('Ctrl Pts',(96.6824242116089,10.9137173667906,9.1184960127668));
#107793=CARTESIAN_POINT('Ctrl Pts',(96.6827531754784,10.925526069197,9.1184960127668));
#107794=CARTESIAN_POINT('Ctrl Pts',(96.6842167271888,10.9780626794681,9.1184960127668));
#107795=CARTESIAN_POINT('Ctrl Pts',(96.6891065426952,11.0304307823436,9.1184960127668));
#107796=CARTESIAN_POINT('Ctrl Pts',(96.6972216454077,11.0824121493641,9.1184960127668));
#107797=CARTESIAN_POINT('Ctrl Pts',(96.701143463069,11.1075333894095,9.1184960127668));
#107798=CARTESIAN_POINT('Ctrl Pts',(96.7058193396968,11.1325644201795,9.1184960127668));
#107799=CARTESIAN_POINT('Ctrl Pts',(96.7112308078138,11.1574808086853,9.1184960127668));
#107800=CARTESIAN_POINT('Ctrl Pts',(96.7146572466834,11.1732573928251,9.1184960127668));
#107801=CARTESIAN_POINT('Ctrl Pts',(96.7183786513777,11.188988014253,9.1184960127668));
#107802=CARTESIAN_POINT('Ctrl Pts',(96.7223908722737,11.2046664142087,9.1184960127668));
#107803=CARTESIAN_POINT('Ctrl Pts',(96.7249070283208,11.2144986995884,9.1184960127668));
#107804=CARTESIAN_POINT('Ctrl Pts',(96.7275377758382,11.2243107938145,9.1184960127668));
#107805=CARTESIAN_POINT('Ctrl Pts',(96.730277664453,11.234086259318,9.1184960127668));
#107806=CARTESIAN_POINT('Ctrl Pts',(96.7450725356843,11.2868718917602,9.1184960127668));
#107807=CARTESIAN_POINT('Ctrl Pts',(96.7630715066882,11.3386947259173,9.1184960127668));
#107808=CARTESIAN_POINT('Ctrl Pts',(96.7840343095851,11.3893192975371,9.1184960127668));
#107809=CARTESIAN_POINT('Ctrl Pts',(96.8054552476105,11.4410502524366,9.1184960127668));
#107810=CARTESIAN_POINT('Ctrl Pts',(96.8299711992107,11.4915309516225,9.1184960127668));
#107811=CARTESIAN_POINT('Ctrl Pts',(96.8573807452556,11.540510511024,9.1184960127668));
#107812=CARTESIAN_POINT('Ctrl Pts',(96.872786221314,11.5680393664262,9.1184960127668));
#107813=CARTESIAN_POINT('Ctrl Pts',(96.8891067425656,11.5950939415267,9.1184960127668));
#107814=CARTESIAN_POINT('Ctrl Pts',(96.906313477585,11.6216279524499,9.1184960127668));
#107815=CARTESIAN_POINT('Ctrl Pts',(96.9175801783897,11.6390020075443,9.1184960127668));
#107816=CARTESIAN_POINT('Ctrl Pts',(96.9292269360609,11.6561528433843,9.1184960127668));
#107817=CARTESIAN_POINT('Ctrl Pts',(96.9412467190239,11.6730669493708,9.1184960127668));
#107818=CARTESIAN_POINT('Ctrl Pts',(96.9473070401079,11.6815949663442,9.1184960127668));
#107819=CARTESIAN_POINT('Ctrl Pts',(96.9534637066899,11.6900648121644,9.1184960127668));
#107820=CARTESIAN_POINT('Ctrl Pts',(96.9597109884959,11.6984681301698,9.1184960127668));
#107821=CARTESIAN_POINT('Ctrl Pts',(96.994439093181,11.7451814554931,9.1184960127668));
#107822=CARTESIAN_POINT('Ctrl Pts',(97.0318543947935,11.7896964276675,9.1184960127668));
#107823=CARTESIAN_POINT('Ctrl Pts',(97.0717283155403,11.8317549554711,9.1184960127668));
#107824=CARTESIAN_POINT('Ctrl Pts',(97.1117071183608,11.8739241116134,9.1184960127668));
#107825=CARTESIAN_POINT('Ctrl Pts',(97.1541579759603,11.9136249543042,9.1184960127668));
#107826=CARTESIAN_POINT('Ctrl Pts',(97.1988995745023,11.950579789157,9.1184960127668));
#107827=CARTESIAN_POINT('Ctrl Pts',(97.2426124503278,11.9866849387207,9.1184960127668));
#107828=CARTESIAN_POINT('Ctrl Pts',(97.2885125610699,12.0201697994727,9.1184960127668));
#107829=CARTESIAN_POINT('Ctrl Pts',(97.3364691156415,12.0507443169141,9.1184960127668));
#107830=CARTESIAN_POINT('Ctrl Pts',(97.3462254661903,12.0569644407883,9.1184960127668));
#107831=CARTESIAN_POINT('Ctrl Pts',(97.3560670415472,12.0630639797634,9.1184960127668));
#107832=CARTESIAN_POINT('Ctrl Pts',(97.3659929054248,12.0690402776369,9.1184960127668));
#107833=CARTESIAN_POINT('Ctrl Pts',(97.3138573448685,9.79064797878733,9.1184960127668));
#107834=CARTESIAN_POINT('Ctrl Pts',(97.6009341668568,9.58815735646046,9.14231467266158));
#107835=CARTESIAN_POINT('Ctrl Pts',(98.4101263498954,9.44342727335157,9.19240375690137));
#107836=CARTESIAN_POINT('Ctrl Pts',(99.3254100117742,10.3356711404167,9.2687632654862));
#107837=CARTESIAN_POINT('Ctrl Pts',(99.0732671457231,11.6313879250538,9.3475745385213));
#107838=CARTESIAN_POINT('Ctrl Pts',(97.8515312358663,12.1307094457997,9.42638581155637));
#107839=CARTESIAN_POINT('Ctrl Pts',(96.9532436972502,11.513168388854,9.4914820078836));
#107840=CARTESIAN_POINT('Ctrl Pts',(96.8238838120166,10.9366557583736,9.5303077798658));
#107841=CARTESIAN_POINT('Ctrl Pts',(96.8240786690275,10.7501410021477,9.54286312750296));
#107842=CARTESIAN_POINT('Origin',(98.,10.75,9.1184960127668));
#107843=CARTESIAN_POINT('',(96.5365,10.75,9.1184960127668));
#107844=CARTESIAN_POINT('Origin',(98.,10.75,9.1184960127668));
#107845=CARTESIAN_POINT('Origin',(98.,10.75,9.1184960127668));
#107846=CARTESIAN_POINT('',(98.6846644245394,9.7917048010816,9.1184960127668));
#107847=CARTESIAN_POINT('Ctrl Pts',(98.6355914804955,12.0706490290142,9.1184960127668));
#107848=CARTESIAN_POINT('Ctrl Pts',(98.6742459232636,12.0476662825293,9.1184960127668));
#107849=CARTESIAN_POINT('Ctrl Pts',(98.7116923833512,12.0228478308923,9.1184960127668));
#107850=CARTESIAN_POINT('Ctrl Pts',(98.7477773097589,11.9961880312021,9.1184960127668));
#107851=CARTESIAN_POINT('Ctrl Pts',(98.7937429792402,11.9622282684151,9.1184960127668));
#107852=CARTESIAN_POINT('Ctrl Pts',(98.837500916529,11.9252809487968,9.1184960127668));
#107853=CARTESIAN_POINT('Ctrl Pts',(98.8789034740481,11.8856482730193,9.1184960127668));
#107854=CARTESIAN_POINT('Ctrl Pts',(98.8946468210008,11.8705779246444,9.1184960127668));
#107855=CARTESIAN_POINT('Ctrl Pts',(98.9100491720406,11.8551190301289,9.1184960127668));
#107856=CARTESIAN_POINT('Ctrl Pts',(98.9251007544373,11.8392874023257,9.1184960127668));
#107857=CARTESIAN_POINT('Ctrl Pts',(98.9339879045998,11.8299396772894,9.1184960127668));
#107858=CARTESIAN_POINT('Ctrl Pts',(98.9427532639398,11.8204612402146,9.1184960127668));
#107859=CARTESIAN_POINT('Ctrl Pts',(98.9513838800037,11.8108678523316,9.1184960127668));
#107860=CARTESIAN_POINT('Ctrl Pts',(98.9898523430754,11.7681081136552,9.1184960127668));
#107861=CARTESIAN_POINT('Ctrl Pts',(99.0257016044828,11.7230111787601,9.1184960127668));
#107862=CARTESIAN_POINT('Ctrl Pts',(99.0587856979425,11.6758909804124,9.1184960127668));
#107863=CARTESIAN_POINT('Ctrl Pts',(99.0810786704322,11.6441400942423,9.1184960127668));
#107864=CARTESIAN_POINT('Ctrl Pts',(99.1021152266029,11.6114698985822,9.1184960127668));
#107865=CARTESIAN_POINT('Ctrl Pts',(99.1218380897891,11.5779721130894,9.1184960127668));
#107866=CARTESIAN_POINT('Ctrl Pts',(99.130375855498,11.5634713663365,9.1184960127668));
#107867=CARTESIAN_POINT('Ctrl Pts',(99.1386673115564,11.5488155114193,9.1184960127668));
#107868=CARTESIAN_POINT('Ctrl Pts',(99.14670717331,11.5340119227266,9.1184960127668));
#107869=CARTESIAN_POINT('Ctrl Pts',(99.1521866210255,11.5239227579214,9.1184960127668));
#107870=CARTESIAN_POINT('Ctrl Pts',(99.1575500455029,11.5137631182504,9.1184960127668));
#107871=CARTESIAN_POINT('Ctrl Pts',(99.1627878257323,11.5035512284172,9.1184960127668));
#107872=CARTESIAN_POINT('Ctrl Pts',(99.188456039613,11.4535069423098,9.1184960127668));
#107873=CARTESIAN_POINT('Ctrl Pts',(99.2111541768037,11.4021318913227,9.1184960127668));
#107874=CARTESIAN_POINT('Ctrl Pts',(99.2307432138167,11.3497164587869,9.1184960127668));
#107875=CARTESIAN_POINT('Ctrl Pts',(99.2498600002804,11.2985646522673,9.1184960127668));
#107876=CARTESIAN_POINT('Ctrl Pts',(99.2660159096322,11.2464209738408,9.1184960127668));
#107877=CARTESIAN_POINT('Ctrl Pts',(99.2790334447493,11.1935494452341,9.1184960127668));
#107878=CARTESIAN_POINT('Ctrl Pts',(99.2869109368667,11.1615545209964,9.1184960127668));
#107879=CARTESIAN_POINT('Ctrl Pts',(99.2936382121067,11.1292930152132,9.1184960127668));
#107880=CARTESIAN_POINT('Ctrl Pts',(99.2991667226112,11.0968247150207,9.1184960127668));
#107881=CARTESIAN_POINT('Ctrl Pts',(99.3033215590753,11.0724238429494,9.1184960127668));
#107882=CARTESIAN_POINT('Ctrl Pts',(99.3067991965717,11.0479061914403,9.1184960127668));
#107883=CARTESIAN_POINT('Ctrl Pts',(99.3095762909331,11.0232979807197,9.1184960127668));
#107884=CARTESIAN_POINT('Ctrl Pts',(99.3106554499975,11.0137354055235,9.1184960127668));
#107885=CARTESIAN_POINT('Ctrl Pts',(99.3116282087408,11.0041638628727,9.1184960127668));
#107886=CARTESIAN_POINT('Ctrl Pts',(99.3124928851242,10.9945927765962,9.1184960127668));
#107887=CARTESIAN_POINT('Ctrl Pts',(99.3172366087752,10.9420845906342,9.1184960127668));
#107888=CARTESIAN_POINT('Ctrl Pts',(99.3187397604984,10.8895172404699,9.1184960127668));
#107889=CARTESIAN_POINT('Ctrl Pts',(99.3168456041743,10.8371362369631,9.1184960127668));
#107890=CARTESIAN_POINT('Ctrl Pts',(99.3164267682064,10.825553746108,9.1184960127668));
#107891=CARTESIAN_POINT('Ctrl Pts',(99.3158416245084,10.8139803933148,9.1184960127668));
#107892=CARTESIAN_POINT('Ctrl Pts',(99.3150881341521,10.8024188959489,9.1184960127668));
#107893=CARTESIAN_POINT('Ctrl Pts',(99.3115311410324,10.7478406704473,9.1184960127668));
#107894=CARTESIAN_POINT('Ctrl Pts',(99.304226566631,10.6935245877712,9.1184960127668));
#107895=CARTESIAN_POINT('Ctrl Pts',(99.2933434227707,10.6397729100594,9.1184960127668));
#107896=CARTESIAN_POINT('Ctrl Pts',(99.2886881485009,10.6167805830786,9.1184960127668));
#107897=CARTESIAN_POINT('Ctrl Pts',(99.2833774775542,10.5938918575654,9.1184960127668));
#107898=CARTESIAN_POINT('Ctrl Pts',(99.2774220930974,10.5711322064764,9.1184960127668));
#107899=CARTESIAN_POINT('Ctrl Pts',(99.2730409956331,10.5543889969661,9.1184960127668));
#107900=CARTESIAN_POINT('Ctrl Pts',(99.2683109576553,10.5377156641035,9.1184960127668));
#107901=CARTESIAN_POINT('Ctrl Pts',(99.2632357869822,10.5211228325942,9.1184960127668));
#107902=CARTESIAN_POINT('Ctrl Pts',(99.2603236688996,10.5116019144236,9.1184960127668));
#107903=CARTESIAN_POINT('Ctrl Pts',(99.2573006399554,10.5021165033124,9.1184960127668));
#107904=CARTESIAN_POINT('Ctrl Pts',(99.2541689602905,10.4926711758706,9.1184960127668));
#107905=CARTESIAN_POINT('Ctrl Pts',(99.2376426939,10.4428269982574,9.1184960127668));
#107906=CARTESIAN_POINT('Ctrl Pts',(99.2180864219794,10.3940707106807,9.1184960127668));
#107907=CARTESIAN_POINT('Ctrl Pts',(99.1956728157365,10.3466608440923,9.1184960127668));
#107908=CARTESIAN_POINT('Ctrl Pts',(99.1733697042633,10.2994846990314,9.1184960127668));
#107909=CARTESIAN_POINT('Ctrl Pts',(99.1482365664014,10.2536408379213,9.1184960127668));
#107910=CARTESIAN_POINT('Ctrl Pts',(99.1204044127404,10.2094167710738,9.1184960127668));
#107911=CARTESIAN_POINT('Ctrl Pts',(99.1064931374631,10.1873123671065,9.1184960127668));
#107912=CARTESIAN_POINT('Ctrl Pts',(99.0919070356358,10.1656132292874,9.1184960127668));
#107913=CARTESIAN_POINT('Ctrl Pts',(99.076659703857,10.1443594016445,9.1184960127668));
#107914=CARTESIAN_POINT('Ctrl Pts',(99.0654152076224,10.1286852765996,9.1184960127668));
#107915=CARTESIAN_POINT('Ctrl Pts',(99.0538110530504,10.1132533986003,9.1184960127668));
#107916=CARTESIAN_POINT('Ctrl Pts',(99.0418521973943,10.0980809672068,9.1184960127668));
#107917=CARTESIAN_POINT('Ctrl Pts',(99.0360652404285,10.0907389430143,9.1184960127668));
#107918=CARTESIAN_POINT('Ctrl Pts',(99.0301957732572,10.083458542508,9.1184960127668));
#107919=CARTESIAN_POINT('Ctrl Pts',(99.0242527358895,10.0762514482787,9.1184960127668));
#107920=CARTESIAN_POINT('Ctrl Pts',(98.9921687683648,10.0373433676301,9.1184960127668));
#107921=CARTESIAN_POINT('Ctrl Pts',(98.9578814680878,10.0004893575788,9.1184960127668));
#107922=CARTESIAN_POINT('Ctrl Pts',(98.9215213654119,9.96594155220527,9.1184960127668));
#107923=CARTESIAN_POINT('Ctrl Pts',(98.8858968563399,9.93209267622934,9.1184960127668));
#107924=CARTESIAN_POINT('Ctrl Pts',(98.8482818182359,9.90045705616418,9.1184960127668));
#107925=CARTESIAN_POINT('Ctrl Pts',(98.8087752824265,9.87131542359124,9.1184960127668));
#107926=CARTESIAN_POINT('Ctrl Pts',(98.769268746617,9.84217379101829,9.1184960127668));
#107927=CARTESIAN_POINT('Ctrl Pts',(98.7278700859694,9.81552546429294,9.1184960127668));
#107928=CARTESIAN_POINT('Ctrl Pts',(98.6846644245395,9.79170480108161,9.1184960127668));
#107929=CARTESIAN_POINT('Origin',(98.,10.75,9.1184960127668));
#107930=CARTESIAN_POINT('Origin',(98.,10.75,8.19412889803065));
#107931=CARTESIAN_POINT('Ctrl Pts',(98.6846644245394,9.79170480108159,9.1184960127668));
#107932=CARTESIAN_POINT('Ctrl Pts',(99.0010205619527,10.0177288832392,9.14476643711183));
#107933=CARTESIAN_POINT('Ctrl Pts',(99.3870316775812,10.8039329633741,9.19730728580188));
#107934=CARTESIAN_POINT('Ctrl Pts',(98.7148371953222,11.9414877424438,9.27611855883697));
#107935=CARTESIAN_POINT('Ctrl Pts',(97.3959638426784,12.0001663543762,9.35492983187205));
#107936=CARTESIAN_POINT('Ctrl Pts',(96.8468201417438,11.2403713725409,9.41093327826995));
#107937=CARTESIAN_POINT('Ctrl Pts',(96.8207258531474,10.8019570759813,9.44066630032281));
#107938=CARTESIAN_POINT('Ctrl Pts',(96.8211250403636,10.7508514088176,9.44412889803065));
#107939=CARTESIAN_POINT('Ctrl Pts',(98.8507802040446,9.55919972522428,8.95351817334586));
#107940=CARTESIAN_POINT('Ctrl Pts',(99.2438918211996,9.840062594456,8.97978859769089));
#107941=CARTESIAN_POINT('Ctrl Pts',(99.7235583614009,10.8170183756298,9.03232944638095));
#107942=CARTESIAN_POINT('Ctrl Pts',(98.8882736025083,12.2305708436141,9.11114071941604));
#107943=CARTESIAN_POINT('Ctrl Pts',(97.2494103873996,12.3034862743618,9.18995199245111));
#107944=CARTESIAN_POINT('Ctrl Pts',(96.2891274572576,10.9748392367607,9.26876326548621));
#107945=CARTESIAN_POINT('Ctrl Pts',(96.8738712604091,9.44231572200386,9.34757453852128));
#107946=CARTESIAN_POINT('Ctrl Pts',(98.4759321306034,9.09133827696001,9.42638581155638));
#107947=CARTESIAN_POINT('Ctrl Pts',(99.6480368958664,10.2383404251759,9.50519708459146));
#107948=CARTESIAN_POINT('Ctrl Pts',(99.3316025376815,11.8475901717513,9.58400835762655));
#107949=CARTESIAN_POINT('Ctrl Pts',(97.8123909963197,12.4654035568644,9.66281963066163));
#107950=CARTESIAN_POINT('Ctrl Pts',(96.4626446905293,11.5338159711112,9.74163090369672));
#107951=CARTESIAN_POINT('Ctrl Pts',(96.5014975453548,9.89424157261291,9.8204421767318));
#107952=CARTESIAN_POINT('Ctrl Pts',(97.8938626320415,9.02762961555281,9.89925344976689));
#107953=CARTESIAN_POINT('Ctrl Pts',(99.38209434996,9.71673178822254,9.97806472280197));
#107954=CARTESIAN_POINT('Ctrl Pts',(99.6219612123826,11.3391263786206,10.0568759958371));
#107955=CARTESIAN_POINT('Ctrl Pts',(98.3968046496415,12.4293967180445,10.1356872688721));
#107956=CARTESIAN_POINT('Ctrl Pts',(96.8132376708772,12.0027660813303,10.2144985419073));
#107957=CARTESIAN_POINT('Ctrl Pts',(96.3016039690137,10.4445845899381,10.2933098149423));
#107958=CARTESIAN_POINT('Ctrl Pts',(97.3240325846763,9.16226714483924,10.3721210879774));
#107959=CARTESIAN_POINT('Ctrl Pts',(98.9570232088569,9.31405633926968,10.4509323610125));
#107960=CARTESIAN_POINT('Ctrl Pts',(99.72559047614,10.7628498886576,10.5297436340476));
#107961=CARTESIAN_POINT('Ctrl Pts',(98.9355322940975,12.2000368716401,10.6085549070827));
#107962=CARTESIAN_POINT('Ctrl Pts',(97.3004622418451,12.3274899473353,10.6873661801177));
#107963=CARTESIAN_POINT('Ctrl Pts',(96.2972439316179,11.0300881631277,10.7661774531528));
#107964=CARTESIAN_POINT('Ctrl Pts',(96.8320260758406,9.47969904384205,10.8449887261879));
#107965=CARTESIAN_POINT('Ctrl Pts',(98.4217710879573,9.07669884453082,10.923799999223));
#107966=CARTESIAN_POINT('Ctrl Pts',(99.6305548240495,10.1850941909808,11.0026112722581));
#107967=CARTESIAN_POINT('Ctrl Pts',(99.3665532878948,11.8037360763359,11.0814225452932));
#107968=CARTESIAN_POINT('Ctrl Pts',(97.8682237019579,12.470599492792,11.1602338183283));
#107969=CARTESIAN_POINT('Ctrl Pts',(96.48891997648,11.5833455284612,11.2390450913634));
#107970=CARTESIAN_POINT('Ctrl Pts',(96.4744868894682,9.94337905006212,11.3178563643984));
#107971=CARTESIAN_POINT('Ctrl Pts',(97.8379610083861,9.03198632936451,11.3966676374335));
#107972=CARTESIAN_POINT('Ctrl Pts',(99.3477955175543,9.67237536676738,11.4754789104686));
#107973=CARTESIAN_POINT('Ctrl Pts',(99.6402447791345,11.286120016238,11.5542901835037));
#107974=CARTESIAN_POINT('Ctrl Pts',(98.451156396063,12.4156186579111,11.6331014565388));
#107975=CARTESIAN_POINT('Ctrl Pts',(96.8545646983056,12.0406609070249,11.7119127295739));
#107976=CARTESIAN_POINT('Ctrl Pts',(96.2925780427725,10.4999242769354,11.790724002609));
#107977=CARTESIAN_POINT('Ctrl Pts',(97.2728062670646,9.18506649276444,11.869535275644));
#107978=CARTESIAN_POINT('Ctrl Pts',(98.9098662667154,9.28372206455016,11.9483465486791));
#107979=CARTESIAN_POINT('Ctrl Pts',(99.7250970230171,10.7067811561831,12.0271578217142));
#107980=CARTESIAN_POINT('Ctrl Pts',(98.9821480412829,12.1688773140378,12.1059690947493));
#107981=CARTESIAN_POINT('Ctrl Pts',(97.3520818961143,12.3493841746056,12.1847803677844));
#107982=CARTESIAN_POINT('Ctrl Pts',(96.3072424645522,11.0852603964275,12.2635916408195));
#107983=CARTESIAN_POINT('Ctrl Pts',(96.7913723940551,9.51831541479055,12.3424029138545));
#107984=CARTESIAN_POINT('Ctrl Pts',(98.3671852964514,9.06387943325478,12.4212141868896));
#107985=CARTESIAN_POINT('Ctrl Pts',(99.6113410909875,10.1324180255,12.5000254599247));
#107986=CARTESIAN_POINT('Ctrl Pts',(99.4000662606059,11.7587824708276,12.5788367329598));
#107987=CARTESIAN_POINT('Ctrl Pts',(97.9241930617252,12.4739724235433,12.6576480059949));
#107988=CARTESIAN_POINT('Ctrl Pts',(96.5167918600261,11.6319984217279,12.73645927903));
#107989=CARTESIAN_POINT('Ctrl Pts',(96.4490862427128,9.99336658252459,12.8152705520651));
#107990=CARTESIAN_POINT('Ctrl Pts',(97.7822307649859,9.03815766515614,12.8940818251002));
#107991=CARTESIAN_POINT('Ctrl Pts',(99.3120735470219,9.6291563119054,12.9728930981352));
#107992=CARTESIAN_POINT('Ctrl Pts',(99.6567966903475,11.2325477982826,13.0517043711703));
#107993=CARTESIAN_POINT('Ctrl Pts',(98.5050317462293,12.4000820027069,13.1305156442054));
#107994=CARTESIAN_POINT('Ctrl Pts',(96.8971011503598,12.0771930507722,13.2093269172405));
#107995=CARTESIAN_POINT('Ctrl Pts',(96.2853546296468,10.5555281038632,13.2881381902756));
#107996=CARTESIAN_POINT('Ctrl Pts',(97.2223480154194,9.20951780908093,13.3669494633107));
#107997=CARTESIAN_POINT('Ctrl Pts',(98.861748088782,9.25493641821538,13.4457607363457));
#107998=CARTESIAN_POINT('Ctrl Pts',(99.7227834757332,10.6507569228509,13.5245720093808));
#107999=CARTESIAN_POINT('Ctrl Pts',(99.0277243461271,12.1362220213605,13.6033832824159));
#108000=CARTESIAN_POINT('Ctrl Pts',(97.4043906860898,12.3695851463718,13.682194555451));
#108001=CARTESIAN_POINT('Ctrl Pts',(96.3190179094369,11.1400880858094,13.7610058284861));
#108002=CARTESIAN_POINT('Ctrl Pts',(96.7520155781748,9.55821310062242,13.8398171015212));
#108003=CARTESIAN_POINT('Ctrl Pts',(98.3121696742768,9.05287884967496,13.9186283745563));
#108004=CARTESIAN_POINT('Ctrl Pts',(99.5905115302468,10.0803156107518,13.9974396475913));
#108005=CARTESIAN_POINT('Ctrl Pts',(99.4319280686622,11.712922398781,14.0762509206264));
#108006=CARTESIAN_POINT('Ctrl Pts',(97.9805929922645,12.4752036805041,14.1550621936615));
#108007=CARTESIAN_POINT('Ctrl Pts',(96.5455179502704,11.680377333606,14.2338734666966));
#108008=CARTESIAN_POINT('Ctrl Pts',(96.4267930226957,10.042776771883,14.3126847397317));
#108009=CARTESIAN_POINT('Ctrl Pts',(97.2912023327567,9.38147568097394,14.3652255884217));
#108010=CARTESIAN_POINT('Ctrl Pts',(97.7682422725578,9.30496691879707,14.3914960127668));
#108011=CARTESIAN_POINT('Ctrl Pts',(98.7954082775428,9.63670141717672,9.00851078648618));
#108012=CARTESIAN_POINT('Ctrl Pts',(99.162934734784,9.89928469071707,9.0347812108312));
#108013=CARTESIAN_POINT('Ctrl Pts',(99.6113828001277,10.8126565715445,9.08732205952127));
#108014=CARTESIAN_POINT('Ctrl Pts',(98.8304614667797,12.1342098098907,9.16613333255634));
#108015=CARTESIAN_POINT('Ctrl Pts',(97.2982615391592,12.2023796343666,9.24494460559143));
#108016=CARTESIAN_POINT('Ctrl Pts',(96.4004773784714,10.9602058665513,9.32375587862652));
#108017=CARTESIAN_POINT('Ctrl Pts',(96.9471638893438,9.52742465776002,9.4025671516616));
#108018=CARTESIAN_POINT('Ctrl Pts',(98.4449567049526,9.19929012466724,9.48137842469669));
#108019=CARTESIAN_POINT('Ctrl Pts',(99.5407765512603,10.2716411252115,9.56018969773177));
#108020=CARTESIAN_POINT('Ctrl Pts',(99.2449369130049,11.7761549385027,9.63900097076687));
#108021=CARTESIAN_POINT('Ctrl Pts',(97.8246012850799,12.3537587404712,9.71781224380194));
#108022=CARTESIAN_POINT('Ctrl Pts',(96.5627014675891,11.4828023248875,9.79662351683703));
#108023=CARTESIAN_POINT('Ctrl Pts',(96.5990256347329,9.94993750032636,9.87543478987212));
#108024=CARTESIAN_POINT('Ctrl Pts',(97.9007704450228,9.13972785888631,9.9542460629072));
#108025=CARTESIAN_POINT('Ctrl Pts',(99.2921425311463,9.78398071010284,10.0330573359423));
#108026=CARTESIAN_POINT('Ctrl Pts',(99.5163979698276,11.3007838520995,10.1118686089774));
#108027=CARTESIAN_POINT('Ctrl Pts',(98.3709791334962,12.3200953600714,10.1906798820125));
#108028=CARTESIAN_POINT('Ctrl Pts',(96.8904765583723,11.9212314252,10.2694911550475));
#108029=CARTESIAN_POINT('Ctrl Pts',(96.412141872636,10.4644621559158,10.3483024280826));
#108030=CARTESIAN_POINT('Ctrl Pts',(97.3680270474777,9.26560267914335,10.4271137011177));
#108031=CARTESIAN_POINT('Ctrl Pts',(98.8947365941362,9.40751287065647,10.5059249741528));
#108032=CARTESIAN_POINT('Ctrl Pts',(99.6132826573136,10.7620135703149,10.5847362471879));
#108033=CARTESIAN_POINT('Ctrl Pts',(98.8746443877,12.1056631018939,10.663547520223));
#108034=CARTESIAN_POINT('Ctrl Pts',(97.3459907498493,12.2248210594066,10.7423587932581));
#108035=CARTESIAN_POINT('Ctrl Pts',(96.4080656026213,11.0118589881787,10.8211700662931));
#108036=CARTESIAN_POINT('Ctrl Pts',(96.9080421443586,9.56237493456568,10.8999813393282));
#108037=CARTESIAN_POINT('Ctrl Pts',(98.3943206635447,9.18560348071698,10.9787926123633));
#108038=CARTESIAN_POINT('Ctrl Pts',(99.5244322774211,10.2218603531326,11.0576038853984));
#108039=CARTESIAN_POINT('Ctrl Pts',(99.2776129389559,11.7351550300284,11.1364151584335));
#108040=CARTESIAN_POINT('Ctrl Pts',(97.8768001914615,12.3586165056458,11.2152264314686));
#108041=CARTESIAN_POINT('Ctrl Pts',(96.5872666606209,11.5291083152149,11.2940377045037));
#108042=CARTESIAN_POINT('Ctrl Pts',(96.5737729323643,9.99587692876494,11.3728489775387));
#108043=CARTESIAN_POINT('Ctrl Pts',(97.8485071060636,9.14380102162829,11.4516602505738));
#108044=CARTESIAN_POINT('Ctrl Pts',(99.2600759937777,9.74251116882779,11.5304715236089));
#108045=CARTESIAN_POINT('Ctrl Pts',(99.5334915743428,11.2512273400872,11.609282796644));
#108046=CARTESIAN_POINT('Ctrl Pts',(98.4217934669718,12.3072140271177,11.6880940696791));
#108047=CARTESIAN_POINT('Ctrl Pts',(96.9291138698029,11.9566599152967,11.7669053427142));
#108048=CARTESIAN_POINT('Ctrl Pts',(96.4037033871018,10.5162001311355,11.8457166157493));
#108049=CARTESIAN_POINT('Ctrl Pts',(97.3201347283301,9.28691816106932,11.9245278887843));
#108050=CARTESIAN_POINT('Ctrl Pts',(98.8506488004328,9.37915286287718,12.0033391618194));
#108051=CARTESIAN_POINT('Ctrl Pts',(99.6128213199474,10.7095939985976,12.0821504348545));
#108052=CARTESIAN_POINT('Ctrl Pts',(98.9182262094195,12.0765315236982,12.1609617078896));
#108053=CARTESIAN_POINT('Ctrl Pts',(97.3942508058477,12.2452903292819,12.2397729809247));
#108054=CARTESIAN_POINT('Ctrl Pts',(96.4174133940031,11.0634404082077,12.3185842539598));
#108055=CARTESIAN_POINT('Ctrl Pts',(96.8700343547427,9.59847800907903,12.3973955269949));
#108056=CARTESIAN_POINT('Ctrl Pts',(98.3432875175056,9.17361840420285,12.4762068000299));
#108057=CARTESIAN_POINT('Ctrl Pts',(99.506469045264,10.1726125475848,12.555018073065));
#108058=CARTESIAN_POINT('Ctrl Pts',(99.3089447632893,11.6931271716501,12.6338293461001));
#108059=CARTESIAN_POINT('Ctrl Pts',(97.9291268580154,12.3617699135724,12.7126406191352));
#108060=CARTESIAN_POINT('Ctrl Pts',(96.6133245387638,11.5745946980042,12.7914518921703));
#108061=CARTESIAN_POINT('Ctrl Pts',(96.5500254537696,10.0426110874884,12.8702631652054));
#108062=CARTESIAN_POINT('Ctrl Pts',(97.7964039932982,9.14957070403135,12.9490744382404));
#108063=CARTESIAN_POINT('Ctrl Pts',(99.2266789413822,9.70210497011587,13.0278857112755));
#108064=CARTESIAN_POINT('Ctrl Pts',(99.5489662258748,11.2011418004784,13.1066969843106));
#108065=CARTESIAN_POINT('Ctrl Pts',(98.4721624098248,12.2926885549735,13.1855082573457));
#108066=CARTESIAN_POINT('Ctrl Pts',(96.9688818920255,11.9908144118339,13.2643195303808));
#108067=CARTESIAN_POINT('Ctrl Pts',(96.3969501004541,10.5681850550808,13.3431308034159));
#108068=CARTESIAN_POINT('Ctrl Pts',(97.2729604865715,9.30977809516568,13.421942076451));
#108069=CARTESIAN_POINT('Ctrl Pts',(98.8056623317227,9.35224069301209,13.5007533494861));
#108070=CARTESIAN_POINT('Ctrl Pts',(99.6106583468889,10.6572160298536,13.5795646225211));
#108071=CARTESIAN_POINT('Ctrl Pts',(98.9608362395547,12.0460015584055,13.6583758955562));
#108072=CARTESIAN_POINT('Ctrl Pts',(97.4431551460489,12.2641765469923,13.7371871685913));
#108073=CARTESIAN_POINT('Ctrl Pts',(96.4284224493248,11.1146997085129,13.8159984416264));
#108074=CARTESIAN_POINT('Ctrl Pts',(96.8332390261959,9.63577900575786,13.8948097146615));
#108075=CARTESIAN_POINT('Ctrl Pts',(98.29185251577,9.16333377934252,13.9736209876966));
#108076=CARTESIAN_POINT('Ctrl Pts',(99.4869951494774,10.1239011509472,14.0524322607317));
#108077=CARTESIAN_POINT('Ctrl Pts',(99.3387328868789,11.6502518429328,14.1312435337667));
#108078=CARTESIAN_POINT('Ctrl Pts',(97.9818560722007,12.3629210357702,14.2100548068018));
#108079=CARTESIAN_POINT('Ctrl Pts',(96.6401810286692,11.6198249311283,14.2888660798369));
#108080=CARTESIAN_POINT('Ctrl Pts',(96.5291831590731,10.0888054787351,14.367677352872));
#108081=CARTESIAN_POINT('Ctrl Pts',(97.337333509938,9.47054431191841,14.4202182015621));
#108082=CARTESIAN_POINT('Ctrl Pts',(97.7833259237631,9.39901502333043,14.4464886259071));
#108083=CARTESIAN_POINT('Ctrl Pts',(98.7400363510412,9.71420310912915,9.06350339962649));
#108084=CARTESIAN_POINT('Ctrl Pts',(99.0819776483683,9.95850678697813,9.08977382397152));
#108085=CARTESIAN_POINT('Ctrl Pts',(99.4992072388545,10.8082947674593,9.14231467266157));
#108086=CARTESIAN_POINT('Ctrl Pts',(98.7726493310509,12.0378487761672,9.22112594569666));
#108087=CARTESIAN_POINT('Ctrl Pts',(97.3471126909189,12.1012729943714,9.29993721873174));
#108088=CARTESIAN_POINT('Ctrl Pts',(96.5118272996849,10.9455724963419,9.37874849176683));
#108089=CARTESIAN_POINT('Ctrl Pts',(97.0204565182787,9.61253359351617,9.45755976480191));
#108090=CARTESIAN_POINT('Ctrl Pts',(98.4139812793017,9.3072419723745,9.536371037837));
#108091=CARTESIAN_POINT('Ctrl Pts',(99.4335162066539,10.304941825247,9.61518231087208));
#108092=CARTESIAN_POINT('Ctrl Pts',(99.1582712883284,11.7047197052541,9.69399358390718));
#108093=CARTESIAN_POINT('Ctrl Pts',(97.8368115738402,12.2421139240781,9.77280485694225));
#108094=CARTESIAN_POINT('Ctrl Pts',(96.6627582446489,11.4317886786638,9.85161612997734));
#108095=CARTESIAN_POINT('Ctrl Pts',(96.6965537241111,10.0056334280398,9.93042740301242));
#108096=CARTESIAN_POINT('Ctrl Pts',(97.907678258004,9.25182610221983,10.0092386760475));
#108097=CARTESIAN_POINT('Ctrl Pts',(99.2021907123328,9.85122963198313,10.0880499490826));
#108098=CARTESIAN_POINT('Ctrl Pts',(99.4108347272724,11.2624413255784,10.1668612221177));
#108099=CARTESIAN_POINT('Ctrl Pts',(98.3451536173513,12.2107940020982,10.2456724951528));
#108100=CARTESIAN_POINT('Ctrl Pts',(96.9677154458671,11.8396967690697,10.3244837681879));
#108101=CARTESIAN_POINT('Ctrl Pts',(96.5226797762587,10.4843397218936,10.4032950412229));
#108102=CARTESIAN_POINT('Ctrl Pts',(97.4120215102787,9.36893821344744,10.482106314258));
#108103=CARTESIAN_POINT('Ctrl Pts',(98.8324499794158,9.50096940204327,10.5609175872931));
#108104=CARTESIAN_POINT('Ctrl Pts',(99.5009748384872,10.7611772519721,10.6397288603282));
#108105=CARTESIAN_POINT('Ctrl Pts',(98.8137564813025,12.0112893321476,10.7185401333633));
#108106=CARTESIAN_POINT('Ctrl Pts',(97.3915192578535,12.1221521714779,10.7973514063984));
#108107=CARTESIAN_POINT('Ctrl Pts',(96.5188872736248,10.9936298132297,10.8761626794335));
#108108=CARTESIAN_POINT('Ctrl Pts',(96.9840582128766,9.64505082528932,10.9549739524685));
#108109=CARTESIAN_POINT('Ctrl Pts',(98.3668702391322,9.29450811690314,11.0337852255036));
#108110=CARTESIAN_POINT('Ctrl Pts',(99.4183097307926,10.2586265152843,11.1125964985387));
#108111=CARTESIAN_POINT('Ctrl Pts',(99.1886725900172,11.6665739837209,11.1914077715738));
#108112=CARTESIAN_POINT('Ctrl Pts',(97.885376680965,12.2466335184996,11.2702190446089));
#108113=CARTESIAN_POINT('Ctrl Pts',(96.685613344762,11.4748711019686,11.349030317644));
#108114=CARTESIAN_POINT('Ctrl Pts',(96.67305897526,10.0483748074678,11.4278415906791));
#108115=CARTESIAN_POINT('Ctrl Pts',(97.8590532037414,9.25561571389206,11.5066528637141));
#108116=CARTESIAN_POINT('Ctrl Pts',(99.1723564700011,9.8126469708882,11.5854641367492));
#108117=CARTESIAN_POINT('Ctrl Pts',(99.4267383695512,11.2163346639364,11.6642754097843));
#108118=CARTESIAN_POINT('Ctrl Pts',(98.3924305378805,12.1988093963244,11.7430866828194));
#108119=CARTESIAN_POINT('Ctrl Pts',(97.0036630413004,11.8726589235686,11.8218979558545));
#108120=CARTESIAN_POINT('Ctrl Pts',(96.514828731431,10.5324759853356,11.9007092288896));
#108121=CARTESIAN_POINT('Ctrl Pts',(97.3674631895958,9.3887698293742,11.9795205019247));
#108122=CARTESIAN_POINT('Ctrl Pts',(98.7914313341501,9.47458366120421,12.0583317749597));
#108123=CARTESIAN_POINT('Ctrl Pts',(99.5005456168779,10.712406841012,12.1371430479948));
#108124=CARTESIAN_POINT('Ctrl Pts',(98.8543043775559,11.9841857333585,12.2159543210299));
#108125=CARTESIAN_POINT('Ctrl Pts',(97.4364197155815,12.1411964839582,12.294765594065));
#108126=CARTESIAN_POINT('Ctrl Pts',(96.5275843234539,11.0416204199878,12.3735768671001));
#108127=CARTESIAN_POINT('Ctrl Pts',(96.9486963154304,9.67864060336751,12.4523881401352));
#108128=CARTESIAN_POINT('Ctrl Pts',(98.31938973856,9.2833573751509,12.5311994131703));
#108129=CARTESIAN_POINT('Ctrl Pts',(99.4015969995403,10.2128070696696,12.6100106862053));
#108130=CARTESIAN_POINT('Ctrl Pts',(99.2178232659729,11.6274718724726,12.6888219592404));
#108131=CARTESIAN_POINT('Ctrl Pts',(97.9340606543056,12.2495674036014,12.7676332322755));
#108132=CARTESIAN_POINT('Ctrl Pts',(96.7098572175013,11.5171909742806,12.8464445053106));
#108133=CARTESIAN_POINT('Ctrl Pts',(96.6509646648264,10.0918555924522,12.9252557783457));
#108134=CARTESIAN_POINT('Ctrl Pts',(97.8105772216106,9.26098374290656,13.0040670513808));
#108135=CARTESIAN_POINT('Ctrl Pts',(99.1412843357424,9.77505362832634,13.0828783244159));
#108136=CARTESIAN_POINT('Ctrl Pts',(99.4411357614023,11.1697358026742,13.1616895974509));
#108137=CARTESIAN_POINT('Ctrl Pts',(98.4392930734199,12.1852951072401,13.240500870486));
#108138=CARTESIAN_POINT('Ctrl Pts',(97.0406626336916,11.9044357728958,13.3193121435211));
#108139=CARTESIAN_POINT('Ctrl Pts',(96.5085455712611,10.5808420062985,13.3981234165562));
#108140=CARTESIAN_POINT('Ctrl Pts',(97.3235729577238,9.41003838125043,13.4769346895913));
#108141=CARTESIAN_POINT('Ctrl Pts',(98.7495765746631,9.44954496780881,13.5557459626264));
#108142=CARTESIAN_POINT('Ctrl Pts',(99.4985332180447,10.6636751368563,13.6345572356615));
#108143=CARTESIAN_POINT('Ctrl Pts',(98.8939481329824,11.9557810954505,13.7133685086965));
#108144=CARTESIAN_POINT('Ctrl Pts',(97.4819196060078,12.1587679476128,13.7921797817316));
#108145=CARTESIAN_POINT('Ctrl Pts',(96.5378269892129,11.0893113312165,13.8709910547667));
#108146=CARTESIAN_POINT('Ctrl Pts',(96.914462474217,9.7133449108933,13.9498023278018));
#108147=CARTESIAN_POINT('Ctrl Pts',(98.271535357263,9.27378870901005,14.0286136008369));
#108148=CARTESIAN_POINT('Ctrl Pts',(99.3834787687081,10.1674866911426,14.107424873872));
#108149=CARTESIAN_POINT('Ctrl Pts',(99.2455377050953,11.5875812870845,14.1862361469071));
#108150=CARTESIAN_POINT('Ctrl Pts',(97.9831191521371,12.2506383910364,14.2650474199421));
#108151=CARTESIAN_POINT('Ctrl Pts',(96.7348441070681,11.5592725286507,14.3438586929772));
#108152=CARTESIAN_POINT('Ctrl Pts',(96.6315732954504,10.1348341855873,14.4226699660123));
#108153=CARTESIAN_POINT('Ctrl Pts',(97.3834646871194,9.55961294286288,14.4752108147024));
#108154=CARTESIAN_POINT('Ctrl Pts',(97.7984095749683,9.4930631278638,14.5014812390474));
#108155=CARTESIAN_POINT('Ctrl Pts',(98.6846644245394,9.79170480108159,9.1184960127668));
#108156=CARTESIAN_POINT('Ctrl Pts',(99.0010205619527,10.0177288832392,9.14476643711183));
#108157=CARTESIAN_POINT('Ctrl Pts',(99.3870316775812,10.8039329633741,9.19730728580188));
#108158=CARTESIAN_POINT('Ctrl Pts',(98.7148371953222,11.9414877424438,9.27611855883697));
#108159=CARTESIAN_POINT('Ctrl Pts',(97.3959638426784,12.0001663543762,9.35492983187205));
#108160=CARTESIAN_POINT('Ctrl Pts',(96.6231772208986,10.9309391261325,9.43374110490715));
#108161=CARTESIAN_POINT('Ctrl Pts',(97.0937491472135,9.69764252927232,9.51255237794222));
#108162=CARTESIAN_POINT('Ctrl Pts',(98.383005853651,9.41519382008176,9.59136365097731));
#108163=CARTESIAN_POINT('Ctrl Pts',(99.3262558620476,10.3382425252825,9.6701749240124));
#108164=CARTESIAN_POINT('Ctrl Pts',(99.0716056636518,11.6332844720055,9.74898619704748));
#108165=CARTESIAN_POINT('Ctrl Pts',(97.8490218626003,12.130469107685,9.82779747008258));
#108166=CARTESIAN_POINT('Ctrl Pts',(96.7628150217088,11.3807750324401,9.90660874311765));
#108167=CARTESIAN_POINT('Ctrl Pts',(96.7940818134893,10.0613293557532,9.98542001615274));
#108168=CARTESIAN_POINT('Ctrl Pts',(97.9145860709853,9.36392434555335,10.0642312891878));
#108169=CARTESIAN_POINT('Ctrl Pts',(99.1122388935191,9.91847855386342,10.1430425622229));
#108170=CARTESIAN_POINT('Ctrl Pts',(99.3052714847173,11.2240987990573,10.221853835258));
#108171=CARTESIAN_POINT('Ctrl Pts',(98.319328101206,12.101492644125,10.3006651082931));
#108172=CARTESIAN_POINT('Ctrl Pts',(97.0449543333623,11.7581621129394,10.3794763813282));
#108173=CARTESIAN_POINT('Ctrl Pts',(96.6332176798809,10.5042172878713,10.4582876543632));
#108174=CARTESIAN_POINT('Ctrl Pts',(97.45601597308,9.47227374775156,10.5370989273983));
#108175=CARTESIAN_POINT('Ctrl Pts',(98.7701633646951,9.59442593343006,10.6159102004334));
#108176=CARTESIAN_POINT('Ctrl Pts',(99.3886670196609,10.7603409336293,10.6947214734685));
#108177=CARTESIAN_POINT('Ctrl Pts',(98.7528685749049,11.9169155624013,10.7735327465036));
#108178=CARTESIAN_POINT('Ctrl Pts',(97.4370477658578,12.0194832835491,10.8523440195387));
#108179=CARTESIAN_POINT('Ctrl Pts',(96.629708944628,10.9754006382806,10.9311552925738));
#108180=CARTESIAN_POINT('Ctrl Pts',(97.0600742813947,9.72772671601295,11.0099665656089));
#108181=CARTESIAN_POINT('Ctrl Pts',(98.3394198147195,9.4034127530893,11.0887778386439));
#108182=CARTESIAN_POINT('Ctrl Pts',(99.3121871841641,10.2953926774361,11.167589111679));
#108183=CARTESIAN_POINT('Ctrl Pts',(99.0997322410784,11.5979929374135,11.2464003847141));
#108184=CARTESIAN_POINT('Ctrl Pts',(97.8939531704686,12.1346505313534,11.3252116577492));
#108185=CARTESIAN_POINT('Ctrl Pts',(96.7839600289029,11.4206338887223,11.4040229307843));
#108186=CARTESIAN_POINT('Ctrl Pts',(96.772345018156,10.1008726861706,11.4828342038194));
#108187=CARTESIAN_POINT('Ctrl Pts',(97.8695993014189,9.36743040615582,11.5616454768545));
#108188=CARTESIAN_POINT('Ctrl Pts',(99.0846369462246,9.88278277294862,11.6404567498895));
#108189=CARTESIAN_POINT('Ctrl Pts',(99.3199851647595,11.1814419877856,11.7192680229246));
#108190=CARTESIAN_POINT('Ctrl Pts',(98.3630676087894,12.0904047655311,11.7980792959597));
#108191=CARTESIAN_POINT('Ctrl Pts',(97.0782122127977,11.7886579318405,11.8768905689948));
#108192=CARTESIAN_POINT('Ctrl Pts',(96.6259540757604,10.5487518395358,11.9557018420299));
#108193=CARTESIAN_POINT('Ctrl Pts',(97.4147916508613,9.49062149767907,12.034513115065));
#108194=CARTESIAN_POINT('Ctrl Pts',(98.7322138678675,9.57001445953124,12.1133243881001));
#108195=CARTESIAN_POINT('Ctrl Pts',(99.3882699138082,10.7152196834265,12.1921356611351));
#108196=CARTESIAN_POINT('Ctrl Pts',(98.7903825456925,11.8918399430189,12.2709469341702));
#108197=CARTESIAN_POINT('Ctrl Pts',(97.478588625315,12.0371026386346,12.3497582072053));
#108198=CARTESIAN_POINT('Ctrl Pts',(96.6377552529049,11.019800431768,12.4285694802404));
#108199=CARTESIAN_POINT('Ctrl Pts',(97.0273582761178,9.758803197656,12.5073807532755));
#108200=CARTESIAN_POINT('Ctrl Pts',(98.2954919596144,9.39309634609896,12.5861920263106));
#108201=CARTESIAN_POINT('Ctrl Pts',(99.2967249538166,10.2530015917544,12.6650032993457));
#108202=CARTESIAN_POINT('Ctrl Pts',(99.1267017686563,11.561816573295,12.7438145723807));
#108203=CARTESIAN_POINT('Ctrl Pts',(97.9389944505958,12.1373648936305,12.8226258454158));
#108204=CARTESIAN_POINT('Ctrl Pts',(96.8063898962389,11.4597872505569,12.9014371184509));
#108205=CARTESIAN_POINT('Ctrl Pts',(96.7519038758833,10.141100097416,12.980248391486));
#108206=CARTESIAN_POINT('Ctrl Pts',(97.8247504499228,9.37239678178178,13.0590596645211));
#108207=CARTESIAN_POINT('Ctrl Pts',(99.0558897301026,9.8480022865368,13.1378709375562));
#108208=CARTESIAN_POINT('Ctrl Pts',(99.3333052969297,11.1383298048701,13.2166822105913));
#108209=CARTESIAN_POINT('Ctrl Pts',(98.4064237370152,12.0779016595067,13.2954934836263));
#108210=CARTESIAN_POINT('Ctrl Pts',(97.1124433753578,11.8180571339576,13.3743047566614));
#108211=CARTESIAN_POINT('Ctrl Pts',(96.620141042068,10.5934989575161,13.4531160296965));
#108212=CARTESIAN_POINT('Ctrl Pts',(97.3741854288762,9.51029866733518,13.5319273027316));
#108213=CARTESIAN_POINT('Ctrl Pts',(98.6934908176036,9.54684924260553,13.6107385757667));
#108214=CARTESIAN_POINT('Ctrl Pts',(99.3864080892004,10.670134243859,13.6895498488018));
#108215=CARTESIAN_POINT('Ctrl Pts',(98.82706002641,11.8655606324956,13.7683611218369));
#108216=CARTESIAN_POINT('Ctrl Pts',(97.5206840659668,12.0533593482333,13.8471723948719));
#108217=CARTESIAN_POINT('Ctrl Pts',(96.6472315291008,11.06392295392,13.925983667907));
#108218=CARTESIAN_POINT('Ctrl Pts',(96.9956859222381,9.79091081602872,14.0047949409421));
#108219=CARTESIAN_POINT('Ctrl Pts',(98.2512181987561,9.38424363867761,14.0836062139772));
#108220=CARTESIAN_POINT('Ctrl Pts',(99.2799623879387,10.2110722313379,14.1624174870123));
#108221=CARTESIAN_POINT('Ctrl Pts',(99.1523425233119,11.5249107312363,14.2412287600474));
#108222=CARTESIAN_POINT('Ctrl Pts',(97.9843822320735,12.1383557463025,14.3200400330825));
#108223=CARTESIAN_POINT('Ctrl Pts',(96.829507185467,11.4987201261731,14.3988513061175));
#108224=CARTESIAN_POINT('Ctrl Pts',(96.7339634318277,10.1808628924395,14.4776625791526));
#108225=CARTESIAN_POINT('Ctrl Pts',(97.4295958643008,9.64868157380735,14.5302034278427));
#108226=CARTESIAN_POINT('Ctrl Pts',(97.8134932261736,9.58711123239716,14.5564738521877));
#108227=CARTESIAN_POINT('Ctrl Pts',(97.7682422725578,9.30496691879707,14.3914960127668));
#108228=CARTESIAN_POINT('Ctrl Pts',(97.2912023327567,9.38147568097394,14.3652255884217));
#108229=CARTESIAN_POINT('Ctrl Pts',(96.8589976777262,9.71212622642846,14.3389551640767));
#108230=CARTESIAN_POINT('Ctrl Pts',(96.6626828381401,10.1503849261096,14.3126847397317));
#108231=CARTESIAN_POINT('Ctrl Pts',(96.5791521581158,10.3368611358961,14.3015068460244));
#108232=CARTESIAN_POINT('Ctrl Pts',(96.5383280749783,10.542819229865,14.290328952317));
#108233=CARTESIAN_POINT('Ctrl Pts',(96.5389396828847,10.7491495099393,14.2791510586097));
#108234=CARTESIAN_POINT('Origin',(98.,10.75,8.95499601276678));
#108235=CARTESIAN_POINT('',(96.9839745962156,10.75,8.85499601276677));
#108236=CARTESIAN_POINT('Origin',(98.,10.75,8.85499601276678));
#108237=CARTESIAN_POINT('',(97.1339745962156,10.75,9.00499601276677));
#108238=CARTESIAN_POINT('',(97.0839745962156,10.75,8.95499601276678));
#108239=CARTESIAN_POINT('',(97.189703570316,10.6534745854044,9.05499601276678));
#108240=CARTESIAN_POINT('Ctrl Pts',(97.189703570316,10.6534745854044,9.05499601276678));
#108241=CARTESIAN_POINT('Ctrl Pts',(97.1626673723677,10.7003026538944,9.03368878891887));
#108242=CARTESIAN_POINT('Ctrl Pts',(97.1339745962156,10.75,9.00499601276677));
#108243=CARTESIAN_POINT('',(97.5112583240073,10.0965254145956,9.05499601276678));
#108244=CARTESIAN_POINT('Origin',(98.,10.75,9.05499601276678));
#108245=CARTESIAN_POINT('',(97.5669872981078,10.,9.00499601276675));
#108246=CARTESIAN_POINT('Ctrl Pts',(97.5669872981078,10.,9.00499601276675));
#108247=CARTESIAN_POINT('Ctrl Pts',(97.5382945219557,10.0496973461057,9.03368878891888));
#108248=CARTESIAN_POINT('Ctrl Pts',(97.5112583240073,10.0965254145956,9.05499601276678));
#108249=CARTESIAN_POINT('',(97.6784452463086,10.,9.05499601276678));
#108250=CARTESIAN_POINT('Ctrl Pts',(97.6784452463086,10.,9.05499601276678));
#108251=CARTESIAN_POINT('Ctrl Pts',(97.624372850412,10.,9.03368878891888));
#108252=CARTESIAN_POINT('Ctrl Pts',(97.5669872981078,10.,9.00499601276675));
#108253=CARTESIAN_POINT('',(98.3215547536914,10.,9.05499601276678));
#108254=CARTESIAN_POINT('Origin',(98.,10.75,9.05499601276678));
#108255=CARTESIAN_POINT('',(98.4330127018922,10.,9.00499601276676));
#108256=CARTESIAN_POINT('Ctrl Pts',(98.4330127018922,10.,9.00499601276676));
#108257=CARTESIAN_POINT('Ctrl Pts',(98.375627149588,10.,9.03368878891888));
#108258=CARTESIAN_POINT('Ctrl Pts',(98.3215547536914,10.,9.05499601276678));
#108259=CARTESIAN_POINT('',(98.4887416759926,10.0965254145956,9.05499601276678));
#108260=CARTESIAN_POINT('Ctrl Pts',(98.4887416759927,10.0965254145956,9.05499601276678));
#108261=CARTESIAN_POINT('Ctrl Pts',(98.4617054780443,10.0496973461056,9.03368878891889));
#108262=CARTESIAN_POINT('Ctrl Pts',(98.4330127018922,10.,9.00499601276676));
#108263=CARTESIAN_POINT('',(98.810296429684,10.6534745854044,9.05499601276678));
#108264=CARTESIAN_POINT('Origin',(98.,10.75,9.05499601276678));
#108265=CARTESIAN_POINT('',(98.8660254037844,10.75,9.00499601276677));
#108266=CARTESIAN_POINT('Ctrl Pts',(98.8660254037844,10.75,9.00499601276677));
#108267=CARTESIAN_POINT('Ctrl Pts',(98.8373326276323,10.7003026538944,9.03368878891888));
#108268=CARTESIAN_POINT('Ctrl Pts',(98.810296429684,10.6534745854044,9.05499601276678));
#108269=CARTESIAN_POINT('',(98.810296429684,10.8465254145956,9.05499601276678));
#108270=CARTESIAN_POINT('Ctrl Pts',(98.810296429684,10.8465254145956,9.05499601276678));
#108271=CARTESIAN_POINT('Ctrl Pts',(98.8373326276323,10.7996973461057,9.03368878891894));
#108272=CARTESIAN_POINT('Ctrl Pts',(98.8660254037844,10.75,9.00499601276677));
#108273=CARTESIAN_POINT('',(98.4887416759926,11.4034745854044,9.05499601276678));
#108274=CARTESIAN_POINT('Origin',(98.,10.75,9.05499601276678));
#108275=CARTESIAN_POINT('',(98.4330127018922,11.5,9.00499601276676));
#108276=CARTESIAN_POINT('Ctrl Pts',(98.4330127018922,11.5,9.00499601276676));
#108277=CARTESIAN_POINT('Ctrl Pts',(98.4617054780443,11.4503026538943,9.03368878891891));
#108278=CARTESIAN_POINT('Ctrl Pts',(98.4887416759926,11.4034745854044,9.05499601276678));
#108279=CARTESIAN_POINT('',(98.3215547536914,11.5,9.05499601276678));
#108280=CARTESIAN_POINT('Ctrl Pts',(98.3215547536914,11.5,9.05499601276678));
#108281=CARTESIAN_POINT('Ctrl Pts',(98.375627149588,11.5,9.03368878891889));
#108282=CARTESIAN_POINT('Ctrl Pts',(98.4330127018922,11.5,9.00499601276676));
#108283=CARTESIAN_POINT('',(97.6784452463086,11.5,9.05499601276678));
#108284=CARTESIAN_POINT('Origin',(98.,10.75,9.05499601276678));
#108285=CARTESIAN_POINT('',(97.5669872981078,11.5,9.00499601276675));
#108286=CARTESIAN_POINT('Ctrl Pts',(97.5669872981078,11.5,9.00499601276675));
#108287=CARTESIAN_POINT('Ctrl Pts',(97.624372850412,11.5,9.03368878891888));
#108288=CARTESIAN_POINT('Ctrl Pts',(97.6784452463086,11.5,9.05499601276678));
#108289=CARTESIAN_POINT('',(97.5112583240073,11.4034745854044,9.05499601276678));
#108290=CARTESIAN_POINT('Ctrl Pts',(97.5112583240073,11.4034745854043,9.05499601276678));
#108291=CARTESIAN_POINT('Ctrl Pts',(97.5382945219557,11.4503026538943,9.03368878891889));
#108292=CARTESIAN_POINT('Ctrl Pts',(97.5669872981078,11.5,9.00499601276675));
#108293=CARTESIAN_POINT('',(97.189703570316,10.8465254145956,9.05499601276678));
#108294=CARTESIAN_POINT('Origin',(98.,10.75,9.05499601276678));
#108295=CARTESIAN_POINT('Ctrl Pts',(97.1339745962156,10.75,9.00499601276677));
#108296=CARTESIAN_POINT('Ctrl Pts',(97.1626673723677,10.7996973461056,9.03368878891887));
#108297=CARTESIAN_POINT('Ctrl Pts',(97.189703570316,10.8465254145956,9.05499601276678));
#108298=CARTESIAN_POINT('Origin',(98.,10.75,8.95499601276678));
#108299=CARTESIAN_POINT('',(98.810296429684,10.6534745854044,8.85499601276678));
#108300=CARTESIAN_POINT('',(98.810296429684,10.6534745854044,8.95499601276678));
#108301=CARTESIAN_POINT('',(98.4887416759926,10.0965254145956,8.85499601276678));
#108302=CARTESIAN_POINT('',(98.4887416759926,10.0965254145956,8.95499601276678));
#108303=CARTESIAN_POINT('Origin',(98.,10.75,8.85499601276678));
#108304=CARTESIAN_POINT('Origin',(98.,10.75,8.95499601276678));
#108305=CARTESIAN_POINT('',(98.4887416759926,11.4034745854044,8.85499601276678));
#108306=CARTESIAN_POINT('',(98.4887416759926,11.4034745854044,8.95499601276678));
#108307=CARTESIAN_POINT('',(98.810296429684,10.8465254145956,8.85499601276678));
#108308=CARTESIAN_POINT('',(98.810296429684,10.8465254145956,8.95499601276678));
#108309=CARTESIAN_POINT('Origin',(98.,10.75,8.85499601276678));
#108310=CARTESIAN_POINT('Origin',(98.,10.75,8.95499601276678));
#108311=CARTESIAN_POINT('',(97.6784452463086,10.,8.85499601276678));
#108312=CARTESIAN_POINT('',(97.6784452463086,10.,8.95499601276678));
#108313=CARTESIAN_POINT('',(98.3215547536914,10.,8.85499601276678));
#108314=CARTESIAN_POINT('Origin',(98.,10.75,8.85499601276678));
#108315=CARTESIAN_POINT('',(98.3215547536914,10.,8.95499601276678));
#108316=CARTESIAN_POINT('Origin',(98.,10.75,8.95499601276678));
#108317=CARTESIAN_POINT('',(97.6784452463086,11.5,8.85499601276678));
#108318=CARTESIAN_POINT('',(97.6784452463086,11.5,8.95499601276678));
#108319=CARTESIAN_POINT('',(98.3215547536914,11.5,8.85499601276678));
#108320=CARTESIAN_POINT('',(98.3215547536914,11.5,8.95499601276678));
#108321=CARTESIAN_POINT('Origin',(98.,10.75,8.85499601276678));
#108322=CARTESIAN_POINT('Origin',(98.,10.75,8.95499601276678));
#108323=CARTESIAN_POINT('',(97.189703570316,10.6534745854044,8.85499601276678));
#108324=CARTESIAN_POINT('',(97.189703570316,10.6534745854044,8.95499601276678));
#108325=CARTESIAN_POINT('',(97.5112583240073,10.0965254145956,8.85499601276678));
#108326=CARTESIAN_POINT('Origin',(98.,10.75,8.85499601276678));
#108327=CARTESIAN_POINT('',(97.5112583240073,10.0965254145956,8.95499601276678));
#108328=CARTESIAN_POINT('Origin',(98.,10.75,8.95499601276678));
#108329=CARTESIAN_POINT('',(97.5112583240073,11.4034745854044,8.85499601276678));
#108330=CARTESIAN_POINT('',(97.5112583240073,11.4034745854044,8.95499601276678));
#108331=CARTESIAN_POINT('',(97.189703570316,10.8465254145956,8.85499601276678));
#108332=CARTESIAN_POINT('Origin',(98.,10.75,8.85499601276678));
#108333=CARTESIAN_POINT('',(97.189703570316,10.8465254145956,8.95499601276678));
#108334=CARTESIAN_POINT('Origin',(98.4330127018922,11.5,8.854996));
#108335=CARTESIAN_POINT('',(98.8165063509461,11.5,8.85499601276678));
#108336=CARTESIAN_POINT('',(98.4330127018922,11.5,10.354996));
#108337=CARTESIAN_POINT('',(98.4330127018922,11.5,8.854996));
#108338=CARTESIAN_POINT('',(97.5669872981078,11.5,10.354996));
#108339=CARTESIAN_POINT('',(98.4330127018922,11.5,10.354996));
#108340=CARTESIAN_POINT('',(97.5669872981078,11.5,8.854996));
#108341=CARTESIAN_POINT('Origin',(98.8660254037844,10.75,8.854996));
#108342=CARTESIAN_POINT('',(98.9077722283114,10.6776923788647,8.85499601276678));
#108343=CARTESIAN_POINT('',(98.8660254037844,10.75,10.354996));
#108344=CARTESIAN_POINT('',(98.8660254037844,10.75,8.854996));
#108345=CARTESIAN_POINT('',(98.8660254037844,10.75,10.354996));
#108346=CARTESIAN_POINT('Origin',(98.4330127018922,10.,8.854996));
#108347=CARTESIAN_POINT('',(98.6912658773653,10.4473076211353,8.85499601276678));
#108348=CARTESIAN_POINT('',(98.4330127018922,10.,10.354996));
#108349=CARTESIAN_POINT('',(98.4330127018922,10.,8.854996));
#108350=CARTESIAN_POINT('',(98.4330127018922,10.,10.354996));
#108351=CARTESIAN_POINT('Origin',(99.2,10.75,8.85499601276678));
#108352=CARTESIAN_POINT('Origin',(99.2,10.75,8.85499601276678));
#108353=CARTESIAN_POINT('Origin',(99.2,10.75,8.85499601276678));
#108354=CARTESIAN_POINT('',(98.3834936490539,10.,8.85499601276678));
#108355=CARTESIAN_POINT('Origin',(99.2,10.75,8.85499601276678));
#108356=CARTESIAN_POINT('Origin',(99.2,10.75,8.85499601276678));
#108357=CARTESIAN_POINT('',(97.3922277716886,10.3026923788647,8.85499601276678));
#108358=CARTESIAN_POINT('Origin',(99.2,10.75,8.85499601276678));
#108359=CARTESIAN_POINT('',(97.6087341226347,11.5723076211353,8.85499601276678));
#108360=CARTESIAN_POINT('Origin',(98.8660254037844,10.75,10.3549960127668));
#108361=CARTESIAN_POINT('',(97.5669872981078,10.,10.354996));
#108362=CARTESIAN_POINT('',(97.5669872981078,10.,10.354996));
#108363=CARTESIAN_POINT('Origin',(98.,10.75,10.3549960127668));
#108364=CARTESIAN_POINT('Origin',(98.8660254037844,10.75,10.3549960127668));
#108365=CARTESIAN_POINT('Origin',(98.,10.75,10.3549960127668));
#108366=CARTESIAN_POINT('Origin',(98.8660254037844,10.75,10.3549960127668));
#108367=CARTESIAN_POINT('Origin',(98.,10.75,10.3549960127668));
#108368=CARTESIAN_POINT('Origin',(98.8660254037844,10.75,10.3549960127668));
#108369=CARTESIAN_POINT('Origin',(98.,10.75,10.3549960127668));
#108370=CARTESIAN_POINT('Origin',(98.8660254037844,10.75,10.3549960127668));
#108371=CARTESIAN_POINT('',(97.1339745962156,10.75,10.354996));
#108372=CARTESIAN_POINT('',(97.5669872981078,11.5,10.354996));
#108373=CARTESIAN_POINT('Origin',(98.,10.75,10.3549960127668));
#108374=CARTESIAN_POINT('Origin',(98.8660254037844,10.75,10.3549960127668));
#108375=CARTESIAN_POINT('',(97.1339745962156,10.75,10.354996));
#108376=CARTESIAN_POINT('Origin',(98.,10.75,10.3549960127668));
#108377=CARTESIAN_POINT('Origin',(98.,10.75,10.3549960127668));
#108378=CARTESIAN_POINT('',(98.,10.75,10.8753565729783));
#108379=CARTESIAN_POINT('',(97.1339745962156,10.75,10.3549960127668));
#108380=CARTESIAN_POINT('Origin',(97.5669872981078,10.,8.854996));
#108381=CARTESIAN_POINT('',(97.5669872981078,10.,8.854996));
#108382=CARTESIAN_POINT('Origin',(97.1339745962156,10.75,8.854996));
#108383=CARTESIAN_POINT('',(97.1339745962156,10.75,8.854996));
#108384=CARTESIAN_POINT('Origin',(97.5669872981078,11.5,8.854996));
#108385=CARTESIAN_POINT('Origin',(99.2,10.75,8.85499601276678));
#108386=CARTESIAN_POINT('',(96.8,10.75,8.85499601276678));
#108387=CARTESIAN_POINT('Origin',(98.,10.75,8.85499601276678));
#108388=CARTESIAN_POINT('Origin',(98.,10.75,9.00499601276678));
#108389=CARTESIAN_POINT('',(96.65,10.75,9.00499601276678));
#108390=CARTESIAN_POINT('Origin',(98.,10.75,11.7549960127668));
#108391=CARTESIAN_POINT('Origin',(98.,10.75,14.3914960127668));
#108392=CARTESIAN_POINT('Origin',(98.,10.75,14.6049960127668));
#108393=CARTESIAN_POINT('',(97.,10.75,14.8549960127668));
#108394=CARTESIAN_POINT('Origin',(98.,10.75,14.8549960127668));
#108395=CARTESIAN_POINT('',(96.75,10.75,14.6049960127668));
#108396=CARTESIAN_POINT('Origin',(98.,10.75,14.8549960127668));
#113959=UNCERTAINTY_MEASURE_WITH_UNIT(LENGTH_MEASURE(0.01),#113985,
'DISTANCE_ACCURACY_VALUE',
'Maximum model space distance between geometric entities at asserted c
onnectivities');
#113964=UNCERTAINTY_MEASURE_WITH_UNIT(LENGTH_MEASURE(0.01),#113985,
'DISTANCE_ACCURACY_VALUE',
'Maximum model space distance between geometric entities at asserted c
onnectivities');
#113979=(
GEOMETRIC_REPRESENTATION_CONTEXT(3)
GLOBAL_UNCERTAINTY_ASSIGNED_CONTEXT((#113959))
GLOBAL_UNIT_ASSIGNED_CONTEXT((#113985,#113987,#113988))
REPRESENTATION_CONTEXT('','3D')
);
#113984=(
GEOMETRIC_REPRESENTATION_CONTEXT(3)
GLOBAL_UNCERTAINTY_ASSIGNED_CONTEXT((#113964))
GLOBAL_UNIT_ASSIGNED_CONTEXT((#113985,#113987,#113988))
REPRESENTATION_CONTEXT('','3D')
);
#113985=(
LENGTH_UNIT()
NAMED_UNIT(*)
SI_UNIT(.MILLI.,.METRE.)
);
#113987=(
NAMED_UNIT(*)
PLANE_ANGLE_UNIT()
SI_UNIT($,.RADIAN.)
);
#113988=(
NAMED_UNIT(*)
SI_UNIT($,.STERADIAN.)
SOLID_ANGLE_UNIT()
);
#114003=SHAPE_DEFINITION_REPRESENTATION(#114022,#114065);
#114022=PRODUCT_DEFINITION_SHAPE('',$,#114085);
#114065=SHAPE_REPRESENTATION('',(#63259),#113979);
#114070=PRODUCT_DEFINITION_CONTEXT('part definition',#114129,'design');
#114085=PRODUCT_DEFINITION('2026-10-05-09-51-27-046',
'ISO 4026 - M3 x 6 - 45H (Gib Adjustment Screw)',#114104,#114070);
#114104=PRODUCT_DEFINITION_FORMATION('',$,#114145);
#114129=APPLICATION_CONTEXT(
'Core Data for Automotive Mechanical Design Process');
#114130=PRODUCT_CONTEXT('part definition',#114129,'mechanical');
#114145=PRODUCT('2026-10-05-09-51-27-046',
'ISO 4026 - M3 x 6 - 45H (Gib Adjustment Screw)',$,(#114130));
#114311=COLOUR_RGB('Black',0.12,0.14,0.17);
#114312=FILL_AREA_STYLE_COLOUR('',#114311);
#114313=FILL_AREA_STYLE('',(#114312));
#114314=SURFACE_STYLE_FILL_AREA(#114313);
#114315=SURFACE_SIDE_STYLE('',(#114314));
#114316=SURFACE_STYLE_USAGE(.BOTH.,#114315);
#114317=PRESENTATION_STYLE_ASSIGNMENT((#114316));
ENDSEC;
END-ISO-10303-21;
